ISO-10303-21;
HEADER;
/* Generated by software containing ST-Developer
 * from STEP Tools, Inc. (www.steptools.com) 
 */

FILE_DESCRIPTION(
/* description */ (''),
/* implementation_level */ '2;1');

FILE_NAME(
/* name */ '09_Hex_Nut_ISO_4032_M10.step',
/* time_stamp */ '2026-10-26T06:13:19-07:00',
/* author */ (''),
/* organization */ (''),
/* preprocessor_version */ 'ST-DEVELOPER v20.2',
/* originating_system */ 'Autodesk Translation Framework v15.15.0.0',
/* authorisation */ '');

FILE_SCHEMA (('AUTOMOTIVE_DESIGN { 1 0 10303 214 3 1 1 }','TECHNICAL_DATA_PACKAGING'));
ENDSEC;

DATA;
#10=MECHANICAL_DESIGN_GEOMETRIC_PRESENTATION_REPRESENTATION('',(#305),#56639);
#265=SHAPE_REPRESENTATION_RELATIONSHIP('SRR','None',#56753,#285);
#285=ADVANCED_BREP_SHAPE_REPRESENTATION('',(#325),#56627);
#305=STYLED_ITEM('',(#56922),#325);
#325=MANIFOLD_SOLID_BREP('Body1',#16957);
#343=B_SPLINE_SURFACE_WITH_KNOTS('',3,3,((#33100,#33101,#33102,#33103,#33104),
(#33105,#33106,#33107,#33108,#33109),(#33110,#33111,#33112,#33113,#33114),
(#33115,#33116,#33117,#33118,#33119)),.UNSPECIFIED.,.F.,.F.,.F.,(4,4),(4,
1,4),(0.,1.),(0.173603820977428,0.583467062619184,1.12995138480819),
 .UNSPECIFIED.);
#344=B_SPLINE_SURFACE_WITH_KNOTS('',3,3,((#33149,#33150,#33151,#33152,#33153),
(#33154,#33155,#33156,#33157,#33158),(#33159,#33160,#33161,#33162,#33163),
(#33164,#33165,#33166,#33167,#33168)),.UNSPECIFIED.,.F.,.F.,.F.,(4,4),(4,
1,4),(0.,1.),(0.173603820977427,0.720088143166436,1.12995138480819),
 .UNSPECIFIED.);
#345=B_SPLINE_SURFACE_WITH_KNOTS('',3,3,((#33238,#33239,#33240,#33241,#33242),
(#33243,#33244,#33245,#33246,#33247),(#33248,#33249,#33250,#33251,#33252),
(#33253,#33254,#33255,#33256,#33257)),.UNSPECIFIED.,.F.,.F.,.F.,(4,4),(4,
1,4),(0.,1.),(0.173603820977428,0.583467062619184,1.12995138480819),
 .UNSPECIFIED.);
#346=B_SPLINE_SURFACE_WITH_KNOTS('',3,3,((#33334,#33335,#33336,#33337,#33338),
(#33339,#33340,#33341,#33342,#33343),(#33344,#33345,#33346,#33347,#33348),
(#33349,#33350,#33351,#33352,#33353)),.UNSPECIFIED.,.F.,.F.,.F.,(4,4),(4,
1,4),(0.,1.),(0.173603820977427,0.720088143166436,1.12995138480819),
 .UNSPECIFIED.);
#347=B_SPLINE_SURFACE_WITH_KNOTS('',3,3,((#33367,#33368,#33369,#33370,#33371),
(#33372,#33373,#33374,#33375,#33376),(#33377,#33378,#33379,#33380,#33381),
(#33382,#33383,#33384,#33385,#33386)),.UNSPECIFIED.,.F.,.F.,.F.,(4,4),(4,
1,4),(0.,1.),(0.173603820977428,0.583467062619184,1.12995138480819),
 .UNSPECIFIED.);
#348=B_SPLINE_SURFACE_WITH_KNOTS('',3,3,((#33408,#33409,#33410,#33411,#33412),
(#33413,#33414,#33415,#33416,#33417),(#33418,#33419,#33420,#33421,#33422),
(#33423,#33424,#33425,#33426,#33427)),.UNSPECIFIED.,.F.,.F.,.F.,(4,4),(4,
1,4),(0.,1.),(0.173603820977428,0.583467062619184,1.12995138480819),
 .UNSPECIFIED.);
#512=FACE_BOUND('',#3188,.T.);
#513=FACE_BOUND('',#3215,.T.);
#597=CONICAL_SURFACE('',#17775,7.580184099288,1.30874388895068);
#598=CONICAL_SURFACE('',#17783,8.83380215351701,1.04669145110647);
#599=CONICAL_SURFACE('',#17784,8.83380215351701,1.04669145110647);
#600=CONICAL_SURFACE('',#17785,8.83380215351701,1.04669145110647);
#601=CONICAL_SURFACE('',#17786,8.83380215351701,1.04669145110647);
#602=CONICAL_SURFACE('',#17787,8.83380215351701,1.04669145110647);
#603=CONICAL_SURFACE('',#17788,8.83380215351701,1.04669145110647);
#604=CONICAL_SURFACE('',#17806,8.83380215351701,1.04669145110647);
#605=CONICAL_SURFACE('',#17808,5.25,0.674740942223553);
#606=CONICAL_SURFACE('',#17813,5.25,0.674740942223554);
#942=CIRCLE('',#17776,7.26300281800529);
#943=CIRCLE('',#17777,7.89736538057071);
#944=CIRCLE('',#17778,7.89736538057071);
#945=CIRCLE('',#17779,7.89736538057071);
#946=CIRCLE('',#17780,7.89736538057071);
#947=CIRCLE('',#17781,7.89736538057071);
#948=CIRCLE('',#17782,7.89736538057071);
#949=CIRCLE('',#17790,5.37);
#950=CIRCLE('',#17807,7.60300281800529);
#951=CIRCLE('',#17809,5.37);
#952=CIRCLE('',#17810,5.05);
#953=CIRCLE('',#17812,5.05);
#1386=CYLINDRICAL_SURFACE('',#17811,5.05);
#1765=(
BOUNDED_CURVE()
B_SPLINE_CURVE(2,(#33362,#33363,#33364),.UNSPECIFIED.,.F.,.F.)
B_SPLINE_CURVE_WITH_KNOTS((3,3),(0.146919729838694,0.206437955014875),
 .UNSPECIFIED.)
CURVE()
GEOMETRIC_REPRESENTATION_ITEM()
RATIONAL_B_SPLINE_CURVE((1.00910808226728,1.00963997887916,1.00910808226728))
REPRESENTATION_ITEM('')
);
#1766=(
BOUNDED_CURVE()
B_SPLINE_CURVE(2,(#33395,#33396,#33397),.UNSPECIFIED.,.F.,.F.)
B_SPLINE_CURVE_WITH_KNOTS((3,3),(0.146919729838686,0.206437955014868),
 .UNSPECIFIED.)
CURVE()
GEOMETRIC_REPRESENTATION_ITEM()
RATIONAL_B_SPLINE_CURVE((1.00910808226729,1.00963997887916,1.00910808226729))
REPRESENTATION_ITEM('')
);
#1767=(
BOUNDED_CURVE()
B_SPLINE_CURVE(2,(#33403,#33404,#33405),.UNSPECIFIED.,.F.,.F.)
B_SPLINE_CURVE_WITH_KNOTS((3,3),(0.146919729838689,0.206437955014871),
 .UNSPECIFIED.)
CURVE()
GEOMETRIC_REPRESENTATION_ITEM()
RATIONAL_B_SPLINE_CURVE((1.00910808226729,1.00963997887917,1.00910808226729))
REPRESENTATION_ITEM('')
);
#1768=(
BOUNDED_CURVE()
B_SPLINE_CURVE(2,(#33436,#33437,#33438),.UNSPECIFIED.,.F.,.F.)
B_SPLINE_CURVE_WITH_KNOTS((3,3),(0.146919729838686,0.206437955014869),
 .UNSPECIFIED.)
CURVE()
GEOMETRIC_REPRESENTATION_ITEM()
RATIONAL_B_SPLINE_CURVE((1.00910808226729,1.00963997887916,1.00910808226729))
REPRESENTATION_ITEM('')
);
#1769=(
BOUNDED_CURVE()
B_SPLINE_CURVE(2,(#33444,#33445,#33446),.UNSPECIFIED.,.F.,.F.)
B_SPLINE_CURVE_WITH_KNOTS((3,3),(0.146919729838686,0.206437955014868),
 .UNSPECIFIED.)
CURVE()
GEOMETRIC_REPRESENTATION_ITEM()
RATIONAL_B_SPLINE_CURVE((1.00910808226729,1.00963997887916,1.00910808226729))
REPRESENTATION_ITEM('')
);
#1770=(
BOUNDED_CURVE()
B_SPLINE_CURVE(2,(#33452,#33453,#33454),.UNSPECIFIED.,.F.,.F.)
B_SPLINE_CURVE_WITH_KNOTS((3,3),(0.146919729838688,0.20643795501487),
 .UNSPECIFIED.)
CURVE()
GEOMETRIC_REPRESENTATION_ITEM()
RATIONAL_B_SPLINE_CURVE((1.00910808226729,1.00963997887916,1.00910808226729))
REPRESENTATION_ITEM('')
);
#1771=(
BOUNDED_CURVE()
B_SPLINE_CURVE(2,(#33458,#33459,#33460),.UNSPECIFIED.,.F.,.F.)
B_SPLINE_CURVE_WITH_KNOTS((3,3),(0.18541928992188,1.11813591586374),
 .UNSPECIFIED.)
CURVE()
GEOMETRIC_REPRESENTATION_ITEM()
RATIONAL_B_SPLINE_CURVE((1.06825177535134,1.21144876302791,1.06825177535134))
REPRESENTATION_ITEM('')
);
#1772=(
BOUNDED_CURVE()
B_SPLINE_CURVE(2,(#33462,#33463,#33464),.UNSPECIFIED.,.F.,.F.)
B_SPLINE_CURVE_WITH_KNOTS((3,3),(0.18541928992188,1.11813591586374),
 .UNSPECIFIED.)
CURVE()
GEOMETRIC_REPRESENTATION_ITEM()
RATIONAL_B_SPLINE_CURVE((1.06825177535134,1.21144876302791,1.06825177535134))
REPRESENTATION_ITEM('')
);
#1773=(
BOUNDED_CURVE()
B_SPLINE_CURVE(2,(#33466,#33467,#33468),.UNSPECIFIED.,.F.,.F.)
B_SPLINE_CURVE_WITH_KNOTS((3,3),(0.18541928992188,1.11813591586374),
 .UNSPECIFIED.)
CURVE()
GEOMETRIC_REPRESENTATION_ITEM()
RATIONAL_B_SPLINE_CURVE((1.06825177535134,1.21144876302791,1.06825177535134))
REPRESENTATION_ITEM('')
);
#1774=(
BOUNDED_CURVE()
B_SPLINE_CURVE(2,(#33474,#33475,#33476),.UNSPECIFIED.,.F.,.F.)
B_SPLINE_CURVE_WITH_KNOTS((3,3),(0.18541928992188,0.651777602892792),
 .UNSPECIFIED.)
CURVE()
GEOMETRIC_REPRESENTATION_ITEM()
RATIONAL_B_SPLINE_CURVE((1.06825177535134,1.13985026918962,1.13985026918963))
REPRESENTATION_ITEM('')
);
#1775=(
BOUNDED_CURVE()
B_SPLINE_CURVE(2,(#33477,#33478,#33479),.UNSPECIFIED.,.F.,.F.)
B_SPLINE_CURVE_WITH_KNOTS((3,3),(0.18541928992188,1.11813591586374),
 .UNSPECIFIED.)
CURVE()
GEOMETRIC_REPRESENTATION_ITEM()
RATIONAL_B_SPLINE_CURVE((1.06825177535134,1.21144876302791,1.06825177535134))
REPRESENTATION_ITEM('')
);
#1776=(
BOUNDED_CURVE()
B_SPLINE_CURVE(2,(#33480,#33481,#33482),.UNSPECIFIED.,.F.,.F.)
B_SPLINE_CURVE_WITH_KNOTS((3,3),(0.18541928992188,1.11813591586374),
 .UNSPECIFIED.)
CURVE()
GEOMETRIC_REPRESENTATION_ITEM()
RATIONAL_B_SPLINE_CURVE((1.06825177535134,1.21144876302791,1.06825177535134))
REPRESENTATION_ITEM('')
);
#1777=(
BOUNDED_CURVE()
B_SPLINE_CURVE(2,(#33483,#33484,#33485),.UNSPECIFIED.,.F.,.F.)
B_SPLINE_CURVE_WITH_KNOTS((3,3),(0.651777602892792,1.11813591586374),
 .UNSPECIFIED.)
CURVE()
GEOMETRIC_REPRESENTATION_ITEM()
RATIONAL_B_SPLINE_CURVE((1.13985026918963,1.13985026918963,1.06825177535134))
REPRESENTATION_ITEM('')
);
#2106=FACE_OUTER_BOUND('',#3177,.T.);
#2107=FACE_OUTER_BOUND('',#3178,.T.);
#2108=FACE_OUTER_BOUND('',#3179,.T.);
#2109=FACE_OUTER_BOUND('',#3180,.T.);
#2110=FACE_OUTER_BOUND('',#3181,.T.);
#2111=FACE_OUTER_BOUND('',#3182,.T.);
#2112=FACE_OUTER_BOUND('',#3183,.T.);
#2113=FACE_OUTER_BOUND('',#3184,.T.);
#2114=FACE_OUTER_BOUND('',#3185,.T.);
#2115=FACE_OUTER_BOUND('',#3186,.T.);
#2116=FACE_OUTER_BOUND('',#3187,.T.);
#2117=FACE_OUTER_BOUND('',#3189,.T.);
#2118=FACE_OUTER_BOUND('',#3190,.T.);
#2119=FACE_OUTER_BOUND('',#3191,.T.);
#2120=FACE_OUTER_BOUND('',#3192,.T.);
#2121=FACE_OUTER_BOUND('',#3193,.T.);
#2122=FACE_OUTER_BOUND('',#3194,.T.);
#2123=FACE_OUTER_BOUND('',#3195,.T.);
#2124=FACE_OUTER_BOUND('',#3196,.T.);
#2125=FACE_OUTER_BOUND('',#3197,.T.);
#2126=FACE_OUTER_BOUND('',#3198,.T.);
#2127=FACE_OUTER_BOUND('',#3199,.T.);
#2128=FACE_OUTER_BOUND('',#3200,.T.);
#2129=FACE_OUTER_BOUND('',#3201,.T.);
#2130=FACE_OUTER_BOUND('',#3202,.T.);
#2131=FACE_OUTER_BOUND('',#3203,.T.);
#2132=FACE_OUTER_BOUND('',#3204,.T.);
#2133=FACE_OUTER_BOUND('',#3205,.T.);
#2134=FACE_OUTER_BOUND('',#3206,.T.);
#2135=FACE_OUTER_BOUND('',#3207,.T.);
#2136=FACE_OUTER_BOUND('',#3208,.T.);
#2137=FACE_OUTER_BOUND('',#3209,.T.);
#2138=FACE_OUTER_BOUND('',#3210,.T.);
#2139=FACE_OUTER_BOUND('',#3211,.T.);
#2140=FACE_OUTER_BOUND('',#3212,.T.);
#2141=FACE_OUTER_BOUND('',#3213,.T.);
#2142=FACE_OUTER_BOUND('',#3214,.T.);
#3177=EDGE_LOOP('',(#12278,#12279,#12280,#12281,#12282,#12283,#12284,#12285,
#12286,#12287,#12288,#12289,#12290,#12291,#12292,#12293));
#3178=EDGE_LOOP('',(#12294,#12295,#12296,#12297,#12298,#12299));
#3179=EDGE_LOOP('',(#12300,#12301,#12302,#12303,#12304,#12305));
#3180=EDGE_LOOP('',(#12306,#12307,#12308));
#3181=EDGE_LOOP('',(#12309,#12310,#12311));
#3182=EDGE_LOOP('',(#12312,#12313,#12314));
#3183=EDGE_LOOP('',(#12315,#12316,#12317));
#3184=EDGE_LOOP('',(#12318,#12319,#12320));
#3185=EDGE_LOOP('',(#12321,#12322,#12323));
#3186=EDGE_LOOP('',(#12324,#12325,#12326,#12327,#12328,#12329));
#3187=EDGE_LOOP('',(#12330));
#3188=EDGE_LOOP('',(#12331));
#3189=EDGE_LOOP('',(#12332,#12333,#12334));
#3190=EDGE_LOOP('',(#12335,#12336,#12337));
#3191=EDGE_LOOP('',(#12338,#12339,#12340));
#3192=EDGE_LOOP('',(#12341,#12342,#12343));
#3193=EDGE_LOOP('',(#12344,#12345,#12346));
#3194=EDGE_LOOP('',(#12347,#12348,#12349));
#3195=EDGE_LOOP('',(#12350,#12351,#12352,#12353,#12354,#12355));
#3196=EDGE_LOOP('',(#12356,#12357,#12358,#12359));
#3197=EDGE_LOOP('',(#12360,#12361,#12362,#12363,#12364,#12365,#12366));
#3198=EDGE_LOOP('',(#12367,#12368,#12369,#12370));
#3199=EDGE_LOOP('',(#12371,#12372,#12373,#12374));
#3200=EDGE_LOOP('',(#12375,#12376,#12377,#12378,#12379,#12380));
#3201=EDGE_LOOP('',(#12381,#12382,#12383,#12384));
#3202=EDGE_LOOP('',(#12385,#12386,#12387,#12388));
#3203=EDGE_LOOP('',(#12389,#12390,#12391,#12392));
#3204=EDGE_LOOP('',(#12393,#12394,#12395,#12396));
#3205=EDGE_LOOP('',(#12397,#12398,#12399,#12400));
#3206=EDGE_LOOP('',(#12401,#12402,#12403,#12404));
#3207=EDGE_LOOP('',(#12405,#12406,#12407,#12408,#12409,#12410,#12411,#12412,
#12413,#12414,#12415,#12416,#12417,#12418,#12419,#12420));
#3208=EDGE_LOOP('',(#12421,#12422,#12423,#12424));
#3209=EDGE_LOOP('',(#12425,#12426,#12427,#12428));
#3210=EDGE_LOOP('',(#12429,#12430,#12431,#12432));
#3211=EDGE_LOOP('',(#12433,#12434,#12435,#12436));
#3212=EDGE_LOOP('',(#12437,#12438,#12439,#12440,#12441));
#3213=EDGE_LOOP('',(#12442,#12443,#12444,#12445));
#3214=EDGE_LOOP('',(#12446));
#3215=EDGE_LOOP('',(#12447));
#4166=LINE('',#32891,#5120);
#4167=LINE('',#33281,#5121);
#4168=LINE('',#33290,#5122);
#4169=LINE('',#33292,#5123);
#4170=LINE('',#33308,#5124);
#4171=LINE('',#33311,#5125);
#4172=LINE('',#33333,#5126);
#4173=LINE('',#33365,#5127);
#4174=LINE('',#33366,#5128);
#4175=LINE('',#33398,#5129);
#4176=LINE('',#33399,#5130);
#4177=LINE('',#33406,#5131);
#4178=LINE('',#33407,#5132);
#4179=LINE('',#33439,#5133);
#4180=LINE('',#33440,#5134);
#4181=LINE('',#33447,#5135);
#4182=LINE('',#33448,#5136);
#4183=LINE('',#33455,#5137);
#4184=LINE('',#33456,#5138);
#4185=LINE('',#33473,#5139);
#4186=LINE('',#33490,#5140);
#4187=LINE('',#33494,#5141);
#4188=LINE('',#33497,#5142);
#5120=VECTOR('',#20228,7.580184099288);
#5121=VECTOR('',#20259,10.);
#5122=VECTOR('',#20262,10.);
#5123=VECTOR('',#20265,10.);
#5124=VECTOR('',#20268,10.);
#5125=VECTOR('',#20271,10.);
#5126=VECTOR('',#20274,10.);
#5127=VECTOR('',#20277,10.);
#5128=VECTOR('',#20278,10.);
#5129=VECTOR('',#20281,10.);
#5130=VECTOR('',#20282,10.);
#5131=VECTOR('',#20285,10.);
#5132=VECTOR('',#20286,10.);
#5133=VECTOR('',#20289,10.);
#5134=VECTOR('',#20290,10.);
#5135=VECTOR('',#20293,10.);
#5136=VECTOR('',#20294,10.);
#5137=VECTOR('',#20297,10.);
#5138=VECTOR('',#20298,10.);
#5139=VECTOR('',#20309,8.83380215351701);
#5140=VECTOR('',#20314,5.25);
#5141=VECTOR('',#20319,5.05);
#5142=VECTOR('',#20324,5.25);
#6017=B_SPLINE_CURVE_WITH_KNOTS('',3,(#32893,#32894,#32895,#32896,#32897,
#32898,#32899,#32900,#32901,#32902,#32903,#32904,#32905,#32906,#32907,#32908,
#32909,#32910,#32911),.UNSPECIFIED.,.F.,.F.,(4,3,3,3,3,3,4),(-0.174178071089695,
-0.154986673198929,-0.114885588774786,-0.0950808983971497,-0.0541575034664912,
-0.015183211178068,0.),.UNSPECIFIED.);
#6018=B_SPLINE_CURVE_WITH_KNOTS('',3,(#32915,#32916,#32917,#32918,#32919,
#32920,#32921,#32922,#32923,#32924,#32925,#32926,#32927,#32928,#32929,#32930,
#32931,#32932,#32933,#32934,#32935,#32936,#32937,#32938,#32939,#32940,#32941,
#32942,#32943,#32944,#32945),.UNSPECIFIED.,.F.,.F.,(4,3,3,3,3,3,3,3,3,3,
4),(-0.34833302504866,-0.308790232636103,-0.273824003014673,-0.230071300138895,
-0.208094185883636,-0.154986673198912,-0.114885588774754,-0.0950808983971323,
-0.0541600893914876,-0.0151890133852294,0.),.UNSPECIFIED.);
#6019=B_SPLINE_CURVE_WITH_KNOTS('',3,(#32949,#32950,#32951,#32952,#32953,
#32954,#32955,#32956,#32957,#32958,#32959,#32960,#32961,#32962,#32963,#32964,
#32965,#32966,#32967,#32968,#32969,#32970,#32971,#32972,#32973,#32974,#32975,
#32976,#32977,#32978,#32979),.UNSPECIFIED.,.F.,.F.,(4,3,3,3,3,3,3,3,3,3,
4),(-0.348333025048798,-0.308790232635593,-0.273824003014727,-0.230071300139576,
-0.208094185883622,-0.154986673198899,-0.11488558877477,-0.0950808983971356,
-0.0541600893922442,-0.0151890133860279,0.),.UNSPECIFIED.);
#6020=B_SPLINE_CURVE_WITH_KNOTS('',3,(#32983,#32984,#32985,#32986,#32987,
#32988,#32989,#32990,#32991,#32992,#32993,#32994,#32995,#32996,#32997,#32998,
#32999,#33000,#33001,#33002,#33003,#33004,#33005,#33006,#33007,#33008,#33009,
#33010,#33011,#33012,#33013),.UNSPECIFIED.,.F.,.F.,(4,3,3,3,3,3,3,3,3,3,
4),(-0.348333025048671,-0.308960696547653,-0.273824003014609,-0.233470249531217,
-0.208094185883577,-0.154986673198894,-0.109241611791192,-0.0950808983971477,
-0.0540895389701423,-0.0149322342172363,0.),.UNSPECIFIED.);
#6021=B_SPLINE_CURVE_WITH_KNOTS('',3,(#33017,#33018,#33019,#33020,#33021,
#33022,#33023,#33024,#33025,#33026,#33027,#33028,#33029,#33030,#33031,#33032,
#33033,#33034,#33035,#33036,#33037,#33038,#33039,#33040,#33041,#33042,#33043,
#33044,#33045,#33046,#33047),.UNSPECIFIED.,.F.,.F.,(4,3,3,3,3,3,3,3,3,3,
4),(-0.348333025048856,-0.308790232636422,-0.273824003014757,-0.230071300137989,
-0.208094185883696,-0.154986673198961,-0.114885588774838,-0.0950808983971696,
-0.0541600893923865,-0.0151890133862364,0.),.UNSPECIFIED.);
#6022=B_SPLINE_CURVE_WITH_KNOTS('',3,(#33051,#33052,#33053,#33054,#33055,
#33056,#33057,#33058,#33059,#33060,#33061,#33062,#33063,#33064,#33065,#33066,
#33067,#33068,#33069,#33070,#33071,#33072,#33073,#33074,#33075,#33076,#33077,
#33078,#33079,#33080,#33081),.UNSPECIFIED.,.F.,.F.,(4,3,3,3,3,3,3,3,3,3,
4),(-0.348333025048835,-0.308963919628448,-0.273824003014722,-0.233470249531327,
-0.208094185883678,-0.154986673198948,-0.10923981221781,-0.0950808983971581,
-0.0540902649808351,-0.0149340303411883,0.),.UNSPECIFIED.);
#6023=B_SPLINE_CURVE_WITH_KNOTS('',3,(#33084,#33085,#33086,#33087,#33088,
#33089,#33090,#33091,#33092,#33093,#33094,#33095,#33096,#33097,#33098,#33099),
 .UNSPECIFIED.,.F.,.F.,(4,3,3,3,3,4),(-0.348333025048838,-0.308789249901995,
-0.273824003014767,-0.230071618690294,-0.208094185883669,-0.174178071089695),
 .UNSPECIFIED.);
#6024=B_SPLINE_CURVE_WITH_KNOTS('',3,(#33121,#33122,#33123,#33124),
 .UNSPECIFIED.,.F.,.F.,(4,4),(0.849509741836718,1.12995138480819),
 .UNSPECIFIED.);
#6025=B_SPLINE_CURVE_WITH_KNOTS('',3,(#33126,#33127,#33128,#33129,#33130,
#33131),.UNSPECIFIED.,.F.,.F.,(4,2,4),(-0.0577179767645,-0.0288553777371,
0.),.UNSPECIFIED.);
#6026=B_SPLINE_CURVE_WITH_KNOTS('',3,(#33133,#33134,#33135,#33136,#33137),
 .UNSPECIFIED.,.F.,.F.,(4,1,4),(-1.12682976866335,-0.583467062619184,-0.176725437122352),
 .UNSPECIFIED.);
#6027=B_SPLINE_CURVE_WITH_KNOTS('',3,(#33139,#33140,#33141,#33142,#33143,
#33144),.UNSPECIFIED.,.F.,.F.,(4,2,4),(-0.0577179733807837,-0.0288622045317409,
0.),.UNSPECIFIED.);
#6028=B_SPLINE_CURVE_WITH_KNOTS('',3,(#33145,#33146,#33147,#33148),
 .UNSPECIFIED.,.F.,.F.,(4,4),(0.173603820977428,0.454045463948879),
 .UNSPECIFIED.);
#6029=B_SPLINE_CURVE_WITH_KNOTS('',3,(#33170,#33171,#33172,#33173),
 .UNSPECIFIED.,.F.,.F.,(4,4),(0.84950974183672,1.12995138480819),
 .UNSPECIFIED.);
#6030=B_SPLINE_CURVE_WITH_KNOTS('',3,(#33175,#33176,#33177,#33178,#33179,
#33180),.UNSPECIFIED.,.F.,.F.,(4,2,4),(-0.0577179767754509,-0.0288553777398763,
0.),.UNSPECIFIED.);
#6031=B_SPLINE_CURVE_WITH_KNOTS('',3,(#33182,#33183,#33184,#33185,#33186),
 .UNSPECIFIED.,.F.,.F.,(4,1,4),(-1.12682976866335,-0.720088143166436,-0.176725437122352),
 .UNSPECIFIED.);
#6032=B_SPLINE_CURVE_WITH_KNOTS('',3,(#33187,#33188,#33189,#33190,#33191,
#33192),.UNSPECIFIED.,.F.,.F.,(4,2,4),(-0.0577179733846878,-0.0288622045324974,
0.),.UNSPECIFIED.);
#6033=B_SPLINE_CURVE_WITH_KNOTS('',3,(#33193,#33194,#33195,#33196),
 .UNSPECIFIED.,.F.,.F.,(4,4),(0.173603820977427,0.454045463948881),
 .UNSPECIFIED.);
#6034=B_SPLINE_CURVE_WITH_KNOTS('',3,(#33199,#33200,#33201,#33202),
 .UNSPECIFIED.,.F.,.F.,(4,4),(0.173603820977428,0.454045463948881),
 .UNSPECIFIED.);
#6035=B_SPLINE_CURVE_WITH_KNOTS('',3,(#33205,#33206,#33207,#33208),
 .UNSPECIFIED.,.F.,.F.,(4,4),(0.173603820977428,0.45404546394888),
 .UNSPECIFIED.);
#6036=B_SPLINE_CURVE_WITH_KNOTS('',3,(#33209,#33210,#33211,#33212),
 .UNSPECIFIED.,.F.,.F.,(4,4),(0.84950974183672,1.12995138480819),
 .UNSPECIFIED.);
#6037=B_SPLINE_CURVE_WITH_KNOTS('',3,(#33215,#33216,#33217,#33218),
 .UNSPECIFIED.,.F.,.F.,(4,4),(0.173603820977428,0.454045463948881),
 .UNSPECIFIED.);
#6038=B_SPLINE_CURVE_WITH_KNOTS('',3,(#33219,#33220,#33221,#33222),
 .UNSPECIFIED.,.F.,.F.,(4,4),(0.849509741836719,1.12995138480819),
 .UNSPECIFIED.);
#6039=B_SPLINE_CURVE_WITH_KNOTS('',3,(#33225,#33226,#33227,#33228),
 .UNSPECIFIED.,.F.,.F.,(4,4),(0.173603820977427,0.45404546394888),
 .UNSPECIFIED.);
#6040=B_SPLINE_CURVE_WITH_KNOTS('',3,(#33229,#33230,#33231,#33232),
 .UNSPECIFIED.,.F.,.F.,(4,4),(0.849509741836718,1.12995138480819),
 .UNSPECIFIED.);
#6041=B_SPLINE_CURVE_WITH_KNOTS('',3,(#33234,#33235,#33236,#33237),
 .UNSPECIFIED.,.F.,.F.,(4,4),(0.849509741836719,1.12995138480819),
 .UNSPECIFIED.);
#6042=B_SPLINE_CURVE_WITH_KNOTS('',3,(#33259,#33260,#33261,#33262,#33263,
#33264),.UNSPECIFIED.,.F.,.F.,(4,2,4),(-0.0577179767668117,-0.0288553777377456,
0.),.UNSPECIFIED.);
#6043=B_SPLINE_CURVE_WITH_KNOTS('',3,(#33266,#33267,#33268,#33269,#33270),
 .UNSPECIFIED.,.F.,.F.,(4,1,4),(-1.12682976866335,-0.583467062619184,-0.176725437122352),
 .UNSPECIFIED.);
#6044=B_SPLINE_CURVE_WITH_KNOTS('',3,(#33271,#33272,#33273,#33274,#33275,
#33276),.UNSPECIFIED.,.F.,.F.,(4,2,4),(-0.0577179733828224,-0.0288622045316709,
0.),.UNSPECIFIED.);
#6045=B_SPLINE_CURVE_WITH_KNOTS('',3,(#33284,#33285,#33286,#33287,#33288,
#33289),.UNSPECIFIED.,.F.,.F.,(4,2,4),(-0.0577179733841313,-0.0288622045319975,
0.),.UNSPECIFIED.);
#6046=B_SPLINE_CURVE_WITH_KNOTS('',3,(#33295,#33296,#33297,#33298,#33299,
#33300),.UNSPECIFIED.,.F.,.F.,(4,2,4),(-0.0577179767666892,-0.0288553777374165,
0.),.UNSPECIFIED.);
#6047=B_SPLINE_CURVE_WITH_KNOTS('',3,(#33302,#33303,#33304,#33305,#33306,
#33307),.UNSPECIFIED.,.F.,.F.,(4,2,4),(-0.0577179733770289,-0.0288622045288615,
0.),.UNSPECIFIED.);
#6048=B_SPLINE_CURVE_WITH_KNOTS('',3,(#33312,#33313,#33314,#33315,#33316,
#33317),.UNSPECIFIED.,.F.,.F.,(4,2,4),(-0.0577179767699769,-0.0288553777383127,
0.),.UNSPECIFIED.);
#6049=B_SPLINE_CURVE_WITH_KNOTS('',3,(#33320,#33321,#33322,#33323,#33324,
#33325),.UNSPECIFIED.,.F.,.F.,(4,2,4),(-0.0577179767634003,-0.0288553777369938,
0.),.UNSPECIFIED.);
#6050=B_SPLINE_CURVE_WITH_KNOTS('',3,(#33327,#33328,#33329,#33330,#33331,
#33332),.UNSPECIFIED.,.F.,.F.,(4,2,4),(-0.0577179733866089,-0.0288622045330813,
0.),.UNSPECIFIED.);
#6051=B_SPLINE_CURVE_WITH_KNOTS('',3,(#33354,#33355,#33356,#33357,#33358),
 .UNSPECIFIED.,.F.,.F.,(4,1,4),(-1.12682976866335,-0.720088143166436,-0.176725437122352),
 .UNSPECIFIED.);
#6052=B_SPLINE_CURVE_WITH_KNOTS('',3,(#33387,#33388,#33389,#33390,#33391),
 .UNSPECIFIED.,.F.,.F.,(4,1,4),(-1.12682976866335,-0.583467062619184,-0.176725437122352),
 .UNSPECIFIED.);
#6053=B_SPLINE_CURVE_WITH_KNOTS('',3,(#33428,#33429,#33430,#33431,#33432),
 .UNSPECIFIED.,.F.,.F.,(4,1,4),(-1.12682976866335,-0.583467062619184,-0.176725437122352),
 .UNSPECIFIED.);
#7199=VERTEX_POINT('',#32888);
#7200=VERTEX_POINT('',#32890);
#7201=VERTEX_POINT('',#32892);
#7202=VERTEX_POINT('',#32912);
#7203=VERTEX_POINT('',#32914);
#7204=VERTEX_POINT('',#32946);
#7205=VERTEX_POINT('',#32948);
#7206=VERTEX_POINT('',#32980);
#7207=VERTEX_POINT('',#32982);
#7208=VERTEX_POINT('',#33014);
#7209=VERTEX_POINT('',#33016);
#7210=VERTEX_POINT('',#33048);
#7211=VERTEX_POINT('',#33050);
#7212=VERTEX_POINT('',#33082);
#7213=VERTEX_POINT('',#33120);
#7214=VERTEX_POINT('',#33125);
#7215=VERTEX_POINT('',#33132);
#7216=VERTEX_POINT('',#33138);
#7217=VERTEX_POINT('',#33169);
#7218=VERTEX_POINT('',#33174);
#7219=VERTEX_POINT('',#33181);
#7220=VERTEX_POINT('',#33204);
#7221=VERTEX_POINT('',#33214);
#7222=VERTEX_POINT('',#33224);
#7223=VERTEX_POINT('',#33258);
#7224=VERTEX_POINT('',#33265);
#7225=VERTEX_POINT('',#33278);
#7226=VERTEX_POINT('',#33283);
#7227=VERTEX_POINT('',#33294);
#7228=VERTEX_POINT('',#33301);
#7229=VERTEX_POINT('',#33310);
#7230=VERTEX_POINT('',#33319);
#7231=VERTEX_POINT('',#33326);
#7232=VERTEX_POINT('',#33360);
#7233=VERTEX_POINT('',#33361);
#7234=VERTEX_POINT('',#33393);
#7235=VERTEX_POINT('',#33394);
#7236=VERTEX_POINT('',#33401);
#7237=VERTEX_POINT('',#33402);
#7238=VERTEX_POINT('',#33434);
#7239=VERTEX_POINT('',#33435);
#7240=VERTEX_POINT('',#33442);
#7241=VERTEX_POINT('',#33443);
#7242=VERTEX_POINT('',#33450);
#7243=VERTEX_POINT('',#33451);
#7244=VERTEX_POINT('',#33470);
#7245=VERTEX_POINT('',#33472);
#7246=VERTEX_POINT('',#33487);
#7247=VERTEX_POINT('',#33489);
#7248=VERTEX_POINT('',#33493);
#9046=EDGE_CURVE('',#7199,#7199,#942,.T.);
#9047=EDGE_CURVE('',#7199,#7200,#4166,.T.);
#9048=EDGE_CURVE('',#7200,#7201,#6017,.T.);
#9049=EDGE_CURVE('',#7201,#7202,#943,.T.);
#9050=EDGE_CURVE('',#7202,#7203,#6018,.T.);
#9051=EDGE_CURVE('',#7203,#7204,#944,.T.);
#9052=EDGE_CURVE('',#7204,#7205,#6019,.T.);
#9053=EDGE_CURVE('',#7205,#7206,#945,.T.);
#9054=EDGE_CURVE('',#7206,#7207,#6020,.T.);
#9055=EDGE_CURVE('',#7207,#7208,#946,.T.);
#9056=EDGE_CURVE('',#7208,#7209,#6021,.T.);
#9057=EDGE_CURVE('',#7209,#7210,#947,.T.);
#9058=EDGE_CURVE('',#7210,#7211,#6022,.T.);
#9059=EDGE_CURVE('',#7211,#7212,#948,.T.);
#9060=EDGE_CURVE('',#7212,#7200,#6023,.T.);
#9061=EDGE_CURVE('',#7208,#7213,#6024,.T.);
#9062=EDGE_CURVE('',#7213,#7214,#6025,.F.);
#9063=EDGE_CURVE('',#7214,#7215,#6026,.T.);
#9064=EDGE_CURVE('',#7215,#7216,#6027,.F.);
#9065=EDGE_CURVE('',#7216,#7209,#6028,.T.);
#9066=EDGE_CURVE('',#7206,#7217,#6029,.T.);
#9067=EDGE_CURVE('',#7217,#7218,#6030,.F.);
#9068=EDGE_CURVE('',#7218,#7219,#6031,.T.);
#9069=EDGE_CURVE('',#7219,#7213,#6032,.F.);
#9070=EDGE_CURVE('',#7213,#7207,#6033,.T.);
#9071=EDGE_CURVE('',#7217,#7205,#6034,.T.);
#9072=EDGE_CURVE('',#7220,#7203,#6035,.T.);
#9073=EDGE_CURVE('',#7204,#7220,#6036,.T.);
#9074=EDGE_CURVE('',#7221,#7201,#6037,.T.);
#9075=EDGE_CURVE('',#7202,#7221,#6038,.T.);
#9076=EDGE_CURVE('',#7222,#7211,#6039,.T.);
#9077=EDGE_CURVE('',#7212,#7222,#6040,.T.);
#9078=EDGE_CURVE('',#7210,#7216,#6041,.T.);
#9079=EDGE_CURVE('',#7220,#7223,#6042,.F.);
#9080=EDGE_CURVE('',#7223,#7224,#6043,.T.);
#9081=EDGE_CURVE('',#7224,#7217,#6044,.F.);
#9082=EDGE_CURVE('',#7225,#7225,#949,.T.);
#9083=EDGE_CURVE('',#7218,#7224,#4167,.T.);
#9084=EDGE_CURVE('',#7226,#7220,#6045,.F.);
#9085=EDGE_CURVE('',#7223,#7226,#4168,.T.);
#9086=EDGE_CURVE('',#7214,#7219,#4169,.T.);
#9087=EDGE_CURVE('',#7221,#7227,#6046,.F.);
#9088=EDGE_CURVE('',#7228,#7221,#6047,.F.);
#9089=EDGE_CURVE('',#7227,#7228,#4170,.T.);
#9090=EDGE_CURVE('',#7229,#7215,#4171,.T.);
#9091=EDGE_CURVE('',#7216,#7229,#6048,.F.);
#9092=EDGE_CURVE('',#7222,#7230,#6049,.F.);
#9093=EDGE_CURVE('',#7231,#7222,#6050,.F.);
#9094=EDGE_CURVE('',#7230,#7231,#4172,.T.);
#9095=EDGE_CURVE('',#7229,#7231,#6051,.T.);
#9096=EDGE_CURVE('',#7232,#7233,#1765,.T.);
#9097=EDGE_CURVE('',#7233,#7230,#4173,.T.);
#9098=EDGE_CURVE('',#7231,#7232,#4174,.T.);
#9099=EDGE_CURVE('',#7230,#7228,#6052,.T.);
#9100=EDGE_CURVE('',#7234,#7235,#1766,.T.);
#9101=EDGE_CURVE('',#7235,#7229,#4175,.T.);
#9102=EDGE_CURVE('',#7215,#7234,#4176,.T.);
#9103=EDGE_CURVE('',#7236,#7237,#1767,.T.);
#9104=EDGE_CURVE('',#7237,#7227,#4177,.T.);
#9105=EDGE_CURVE('',#7228,#7236,#4178,.T.);
#9106=EDGE_CURVE('',#7227,#7226,#6053,.T.);
#9107=EDGE_CURVE('',#7238,#7239,#1768,.T.);
#9108=EDGE_CURVE('',#7239,#7214,#4179,.T.);
#9109=EDGE_CURVE('',#7219,#7238,#4180,.T.);
#9110=EDGE_CURVE('',#7240,#7241,#1769,.T.);
#9111=EDGE_CURVE('',#7241,#7223,#4181,.T.);
#9112=EDGE_CURVE('',#7226,#7240,#4182,.T.);
#9113=EDGE_CURVE('',#7242,#7243,#1770,.T.);
#9114=EDGE_CURVE('',#7243,#7218,#4183,.T.);
#9115=EDGE_CURVE('',#7224,#7242,#4184,.T.);
#9116=EDGE_CURVE('',#7239,#7234,#1771,.T.);
#9117=EDGE_CURVE('',#7243,#7238,#1772,.T.);
#9118=EDGE_CURVE('',#7241,#7242,#1773,.T.);
#9119=EDGE_CURVE('',#7244,#7244,#950,.T.);
#9120=EDGE_CURVE('',#7244,#7245,#4185,.T.);
#9121=EDGE_CURVE('',#7233,#7245,#1774,.T.);
#9122=EDGE_CURVE('',#7235,#7232,#1775,.T.);
#9123=EDGE_CURVE('',#7237,#7240,#1776,.T.);
#9124=EDGE_CURVE('',#7245,#7236,#1777,.T.);
#9125=EDGE_CURVE('',#7246,#7246,#951,.T.);
#9126=EDGE_CURVE('',#7246,#7247,#4186,.T.);
#9127=EDGE_CURVE('',#7247,#7247,#952,.T.);
#9128=EDGE_CURVE('',#7247,#7248,#4187,.T.);
#9129=EDGE_CURVE('',#7248,#7248,#953,.T.);
#9130=EDGE_CURVE('',#7248,#7225,#4188,.T.);
#12278=ORIENTED_EDGE('',*,*,#9046,.T.);
#12279=ORIENTED_EDGE('',*,*,#9047,.T.);
#12280=ORIENTED_EDGE('',*,*,#9048,.T.);
#12281=ORIENTED_EDGE('',*,*,#9049,.T.);
#12282=ORIENTED_EDGE('',*,*,#9050,.T.);
#12283=ORIENTED_EDGE('',*,*,#9051,.T.);
#12284=ORIENTED_EDGE('',*,*,#9052,.T.);
#12285=ORIENTED_EDGE('',*,*,#9053,.T.);
#12286=ORIENTED_EDGE('',*,*,#9054,.T.);
#12287=ORIENTED_EDGE('',*,*,#9055,.T.);
#12288=ORIENTED_EDGE('',*,*,#9056,.T.);
#12289=ORIENTED_EDGE('',*,*,#9057,.T.);
#12290=ORIENTED_EDGE('',*,*,#9058,.T.);
#12291=ORIENTED_EDGE('',*,*,#9059,.T.);
#12292=ORIENTED_EDGE('',*,*,#9060,.T.);
#12293=ORIENTED_EDGE('',*,*,#9047,.F.);
#12294=ORIENTED_EDGE('',*,*,#9056,.F.);
#12295=ORIENTED_EDGE('',*,*,#9061,.T.);
#12296=ORIENTED_EDGE('',*,*,#9062,.T.);
#12297=ORIENTED_EDGE('',*,*,#9063,.T.);
#12298=ORIENTED_EDGE('',*,*,#9064,.T.);
#12299=ORIENTED_EDGE('',*,*,#9065,.T.);
#12300=ORIENTED_EDGE('',*,*,#9054,.F.);
#12301=ORIENTED_EDGE('',*,*,#9066,.T.);
#12302=ORIENTED_EDGE('',*,*,#9067,.T.);
#12303=ORIENTED_EDGE('',*,*,#9068,.T.);
#12304=ORIENTED_EDGE('',*,*,#9069,.T.);
#12305=ORIENTED_EDGE('',*,*,#9070,.T.);
#12306=ORIENTED_EDGE('',*,*,#9055,.F.);
#12307=ORIENTED_EDGE('',*,*,#9070,.F.);
#12308=ORIENTED_EDGE('',*,*,#9061,.F.);
#12309=ORIENTED_EDGE('',*,*,#9053,.F.);
#12310=ORIENTED_EDGE('',*,*,#9071,.F.);
#12311=ORIENTED_EDGE('',*,*,#9066,.F.);
#12312=ORIENTED_EDGE('',*,*,#9051,.F.);
#12313=ORIENTED_EDGE('',*,*,#9072,.F.);
#12314=ORIENTED_EDGE('',*,*,#9073,.F.);
#12315=ORIENTED_EDGE('',*,*,#9049,.F.);
#12316=ORIENTED_EDGE('',*,*,#9074,.F.);
#12317=ORIENTED_EDGE('',*,*,#9075,.F.);
#12318=ORIENTED_EDGE('',*,*,#9059,.F.);
#12319=ORIENTED_EDGE('',*,*,#9076,.F.);
#12320=ORIENTED_EDGE('',*,*,#9077,.F.);
#12321=ORIENTED_EDGE('',*,*,#9057,.F.);
#12322=ORIENTED_EDGE('',*,*,#9065,.F.);
#12323=ORIENTED_EDGE('',*,*,#9078,.F.);
#12324=ORIENTED_EDGE('',*,*,#9052,.F.);
#12325=ORIENTED_EDGE('',*,*,#9073,.T.);
#12326=ORIENTED_EDGE('',*,*,#9079,.T.);
#12327=ORIENTED_EDGE('',*,*,#9080,.T.);
#12328=ORIENTED_EDGE('',*,*,#9081,.T.);
#12329=ORIENTED_EDGE('',*,*,#9071,.T.);
#12330=ORIENTED_EDGE('',*,*,#9046,.F.);
#12331=ORIENTED_EDGE('',*,*,#9082,.T.);
#12332=ORIENTED_EDGE('',*,*,#9083,.F.);
#12333=ORIENTED_EDGE('',*,*,#9067,.F.);
#12334=ORIENTED_EDGE('',*,*,#9081,.F.);
#12335=ORIENTED_EDGE('',*,*,#9079,.F.);
#12336=ORIENTED_EDGE('',*,*,#9084,.F.);
#12337=ORIENTED_EDGE('',*,*,#9085,.F.);
#12338=ORIENTED_EDGE('',*,*,#9086,.F.);
#12339=ORIENTED_EDGE('',*,*,#9062,.F.);
#12340=ORIENTED_EDGE('',*,*,#9069,.F.);
#12341=ORIENTED_EDGE('',*,*,#9087,.F.);
#12342=ORIENTED_EDGE('',*,*,#9088,.F.);
#12343=ORIENTED_EDGE('',*,*,#9089,.F.);
#12344=ORIENTED_EDGE('',*,*,#9090,.F.);
#12345=ORIENTED_EDGE('',*,*,#9091,.F.);
#12346=ORIENTED_EDGE('',*,*,#9064,.F.);
#12347=ORIENTED_EDGE('',*,*,#9092,.F.);
#12348=ORIENTED_EDGE('',*,*,#9093,.F.);
#12349=ORIENTED_EDGE('',*,*,#9094,.F.);
#12350=ORIENTED_EDGE('',*,*,#9058,.F.);
#12351=ORIENTED_EDGE('',*,*,#9078,.T.);
#12352=ORIENTED_EDGE('',*,*,#9091,.T.);
#12353=ORIENTED_EDGE('',*,*,#9095,.T.);
#12354=ORIENTED_EDGE('',*,*,#9093,.T.);
#12355=ORIENTED_EDGE('',*,*,#9076,.T.);
#12356=ORIENTED_EDGE('',*,*,#9096,.T.);
#12357=ORIENTED_EDGE('',*,*,#9097,.T.);
#12358=ORIENTED_EDGE('',*,*,#9094,.T.);
#12359=ORIENTED_EDGE('',*,*,#9098,.T.);
#12360=ORIENTED_EDGE('',*,*,#9060,.F.);
#12361=ORIENTED_EDGE('',*,*,#9077,.T.);
#12362=ORIENTED_EDGE('',*,*,#9092,.T.);
#12363=ORIENTED_EDGE('',*,*,#9099,.T.);
#12364=ORIENTED_EDGE('',*,*,#9088,.T.);
#12365=ORIENTED_EDGE('',*,*,#9074,.T.);
#12366=ORIENTED_EDGE('',*,*,#9048,.F.);
#12367=ORIENTED_EDGE('',*,*,#9100,.T.);
#12368=ORIENTED_EDGE('',*,*,#9101,.T.);
#12369=ORIENTED_EDGE('',*,*,#9090,.T.);
#12370=ORIENTED_EDGE('',*,*,#9102,.T.);
#12371=ORIENTED_EDGE('',*,*,#9103,.T.);
#12372=ORIENTED_EDGE('',*,*,#9104,.T.);
#12373=ORIENTED_EDGE('',*,*,#9089,.T.);
#12374=ORIENTED_EDGE('',*,*,#9105,.T.);
#12375=ORIENTED_EDGE('',*,*,#9050,.F.);
#12376=ORIENTED_EDGE('',*,*,#9075,.T.);
#12377=ORIENTED_EDGE('',*,*,#9087,.T.);
#12378=ORIENTED_EDGE('',*,*,#9106,.T.);
#12379=ORIENTED_EDGE('',*,*,#9084,.T.);
#12380=ORIENTED_EDGE('',*,*,#9072,.T.);
#12381=ORIENTED_EDGE('',*,*,#9107,.T.);
#12382=ORIENTED_EDGE('',*,*,#9108,.T.);
#12383=ORIENTED_EDGE('',*,*,#9086,.T.);
#12384=ORIENTED_EDGE('',*,*,#9109,.T.);
#12385=ORIENTED_EDGE('',*,*,#9110,.T.);
#12386=ORIENTED_EDGE('',*,*,#9111,.T.);
#12387=ORIENTED_EDGE('',*,*,#9085,.T.);
#12388=ORIENTED_EDGE('',*,*,#9112,.T.);
#12389=ORIENTED_EDGE('',*,*,#9113,.T.);
#12390=ORIENTED_EDGE('',*,*,#9114,.T.);
#12391=ORIENTED_EDGE('',*,*,#9083,.T.);
#12392=ORIENTED_EDGE('',*,*,#9115,.T.);
#12393=ORIENTED_EDGE('',*,*,#9102,.F.);
#12394=ORIENTED_EDGE('',*,*,#9063,.F.);
#12395=ORIENTED_EDGE('',*,*,#9108,.F.);
#12396=ORIENTED_EDGE('',*,*,#9116,.T.);
#12397=ORIENTED_EDGE('',*,*,#9109,.F.);
#12398=ORIENTED_EDGE('',*,*,#9068,.F.);
#12399=ORIENTED_EDGE('',*,*,#9114,.F.);
#12400=ORIENTED_EDGE('',*,*,#9117,.T.);
#12401=ORIENTED_EDGE('',*,*,#9115,.F.);
#12402=ORIENTED_EDGE('',*,*,#9080,.F.);
#12403=ORIENTED_EDGE('',*,*,#9111,.F.);
#12404=ORIENTED_EDGE('',*,*,#9118,.T.);
#12405=ORIENTED_EDGE('',*,*,#9119,.F.);
#12406=ORIENTED_EDGE('',*,*,#9120,.T.);
#12407=ORIENTED_EDGE('',*,*,#9121,.F.);
#12408=ORIENTED_EDGE('',*,*,#9096,.F.);
#12409=ORIENTED_EDGE('',*,*,#9122,.F.);
#12410=ORIENTED_EDGE('',*,*,#9100,.F.);
#12411=ORIENTED_EDGE('',*,*,#9116,.F.);
#12412=ORIENTED_EDGE('',*,*,#9107,.F.);
#12413=ORIENTED_EDGE('',*,*,#9117,.F.);
#12414=ORIENTED_EDGE('',*,*,#9113,.F.);
#12415=ORIENTED_EDGE('',*,*,#9118,.F.);
#12416=ORIENTED_EDGE('',*,*,#9110,.F.);
#12417=ORIENTED_EDGE('',*,*,#9123,.F.);
#12418=ORIENTED_EDGE('',*,*,#9103,.F.);
#12419=ORIENTED_EDGE('',*,*,#9124,.F.);
#12420=ORIENTED_EDGE('',*,*,#9120,.F.);
#12421=ORIENTED_EDGE('',*,*,#9125,.F.);
#12422=ORIENTED_EDGE('',*,*,#9126,.T.);
#12423=ORIENTED_EDGE('',*,*,#9127,.T.);
#12424=ORIENTED_EDGE('',*,*,#9126,.F.);
#12425=ORIENTED_EDGE('',*,*,#9127,.F.);
#12426=ORIENTED_EDGE('',*,*,#9128,.T.);
#12427=ORIENTED_EDGE('',*,*,#9129,.T.);
#12428=ORIENTED_EDGE('',*,*,#9128,.F.);
#12429=ORIENTED_EDGE('',*,*,#9129,.F.);
#12430=ORIENTED_EDGE('',*,*,#9130,.T.);
#12431=ORIENTED_EDGE('',*,*,#9082,.F.);
#12432=ORIENTED_EDGE('',*,*,#9130,.F.);
#12433=ORIENTED_EDGE('',*,*,#9104,.F.);
#12434=ORIENTED_EDGE('',*,*,#9123,.T.);
#12435=ORIENTED_EDGE('',*,*,#9112,.F.);
#12436=ORIENTED_EDGE('',*,*,#9106,.F.);
#12437=ORIENTED_EDGE('',*,*,#9097,.F.);
#12438=ORIENTED_EDGE('',*,*,#9121,.T.);
#12439=ORIENTED_EDGE('',*,*,#9124,.T.);
#12440=ORIENTED_EDGE('',*,*,#9105,.F.);
#12441=ORIENTED_EDGE('',*,*,#9099,.F.);
#12442=ORIENTED_EDGE('',*,*,#9101,.F.);
#12443=ORIENTED_EDGE('',*,*,#9122,.T.);
#12444=ORIENTED_EDGE('',*,*,#9098,.F.);
#12445=ORIENTED_EDGE('',*,*,#9095,.F.);
#12446=ORIENTED_EDGE('',*,*,#9119,.T.);
#12447=ORIENTED_EDGE('',*,*,#9125,.T.);
#15789=PLANE('',#17789);
#15790=PLANE('',#17791);
#15791=PLANE('',#17792);
#15792=PLANE('',#17793);
#15793=PLANE('',#17794);
#15794=PLANE('',#17795);
#15795=PLANE('',#17796);
#15796=PLANE('',#17797);
#15797=PLANE('',#17798);
#15798=PLANE('',#17799);
#15799=PLANE('',#17800);
#15800=PLANE('',#17801);
#15801=PLANE('',#17802);
#15802=PLANE('',#17803);
#15803=PLANE('',#17804);
#15804=PLANE('',#17805);
#15805=PLANE('',#17814);
#15806=PLANE('',#17815);
#15807=PLANE('',#17816);
#15808=PLANE('',#17817);
#16277=ADVANCED_FACE('',(#2106),#597,.T.);
#16278=ADVANCED_FACE('',(#2107),#343,.T.);
#16279=ADVANCED_FACE('',(#2108),#344,.T.);
#16280=ADVANCED_FACE('',(#2109),#598,.T.);
#16281=ADVANCED_FACE('',(#2110),#599,.T.);
#16282=ADVANCED_FACE('',(#2111),#600,.T.);
#16283=ADVANCED_FACE('',(#2112),#601,.T.);
#16284=ADVANCED_FACE('',(#2113),#602,.T.);
#16285=ADVANCED_FACE('',(#2114),#603,.T.);
#16286=ADVANCED_FACE('',(#2115),#345,.T.);
#16287=ADVANCED_FACE('',(#2116,#512),#15789,.T.);
#16288=ADVANCED_FACE('',(#2117),#15790,.T.);
#16289=ADVANCED_FACE('',(#2118),#15791,.T.);
#16290=ADVANCED_FACE('',(#2119),#15792,.T.);
#16291=ADVANCED_FACE('',(#2120),#15793,.T.);
#16292=ADVANCED_FACE('',(#2121),#15794,.T.);
#16293=ADVANCED_FACE('',(#2122),#15795,.T.);
#16294=ADVANCED_FACE('',(#2123),#346,.T.);
#16295=ADVANCED_FACE('',(#2124),#15796,.T.);
#16296=ADVANCED_FACE('',(#2125),#347,.T.);
#16297=ADVANCED_FACE('',(#2126),#15797,.T.);
#16298=ADVANCED_FACE('',(#2127),#15798,.T.);
#16299=ADVANCED_FACE('',(#2128),#348,.T.);
#16300=ADVANCED_FACE('',(#2129),#15799,.T.);
#16301=ADVANCED_FACE('',(#2130),#15800,.T.);
#16302=ADVANCED_FACE('',(#2131),#15801,.T.);
#16303=ADVANCED_FACE('',(#2132),#15802,.T.);
#16304=ADVANCED_FACE('',(#2133),#15803,.T.);
#16305=ADVANCED_FACE('',(#2134),#15804,.T.);
#16306=ADVANCED_FACE('',(#2135),#604,.T.);
#16307=ADVANCED_FACE('',(#2136),#605,.F.);
#16308=ADVANCED_FACE('',(#2137),#1386,.F.);
#16309=ADVANCED_FACE('',(#2138),#606,.F.);
#16310=ADVANCED_FACE('',(#2139),#15805,.T.);
#16311=ADVANCED_FACE('',(#2140),#15806,.T.);
#16312=ADVANCED_FACE('',(#2141),#15807,.T.);
#16313=ADVANCED_FACE('',(#2142,#513),#15808,.F.);
#16957=CLOSED_SHELL('',(#16277,#16278,#16279,#16280,#16281,#16282,#16283,
#16284,#16285,#16286,#16287,#16288,#16289,#16290,#16291,#16292,#16293,#16294,
#16295,#16296,#16297,#16298,#16299,#16300,#16301,#16302,#16303,#16304,#16305,
#16306,#16307,#16308,#16309,#16310,#16311,#16312,#16313));
#17774=AXIS2_PLACEMENT_3D('',#32886,#20222,#20223);
#17775=AXIS2_PLACEMENT_3D('',#32887,#20224,#20225);
#17776=AXIS2_PLACEMENT_3D('',#32889,#20226,#20227);
#17777=AXIS2_PLACEMENT_3D('',#32913,#20229,#20230);
#17778=AXIS2_PLACEMENT_3D('',#32947,#20231,#20232);
#17779=AXIS2_PLACEMENT_3D('',#32981,#20233,#20234);
#17780=AXIS2_PLACEMENT_3D('',#33015,#20235,#20236);
#17781=AXIS2_PLACEMENT_3D('',#33049,#20237,#20238);
#17782=AXIS2_PLACEMENT_3D('',#33083,#20239,#20240);
#17783=AXIS2_PLACEMENT_3D('',#33197,#20241,#20242);
#17784=AXIS2_PLACEMENT_3D('',#33198,#20243,#20244);
#17785=AXIS2_PLACEMENT_3D('',#33203,#20245,#20246);
#17786=AXIS2_PLACEMENT_3D('',#33213,#20247,#20248);
#17787=AXIS2_PLACEMENT_3D('',#33223,#20249,#20250);
#17788=AXIS2_PLACEMENT_3D('',#33233,#20251,#20252);
#17789=AXIS2_PLACEMENT_3D('',#33277,#20253,#20254);
#17790=AXIS2_PLACEMENT_3D('',#33279,#20255,#20256);
#17791=AXIS2_PLACEMENT_3D('',#33280,#20257,#20258);
#17792=AXIS2_PLACEMENT_3D('',#33282,#20260,#20261);
#17793=AXIS2_PLACEMENT_3D('',#33291,#20263,#20264);
#17794=AXIS2_PLACEMENT_3D('',#33293,#20266,#20267);
#17795=AXIS2_PLACEMENT_3D('',#33309,#20269,#20270);
#17796=AXIS2_PLACEMENT_3D('',#33318,#20272,#20273);
#17797=AXIS2_PLACEMENT_3D('',#33359,#20275,#20276);
#17798=AXIS2_PLACEMENT_3D('',#33392,#20279,#20280);
#17799=AXIS2_PLACEMENT_3D('',#33400,#20283,#20284);
#17800=AXIS2_PLACEMENT_3D('',#33433,#20287,#20288);
#17801=AXIS2_PLACEMENT_3D('',#33441,#20291,#20292);
#17802=AXIS2_PLACEMENT_3D('',#33449,#20295,#20296);
#17803=AXIS2_PLACEMENT_3D('',#33457,#20299,#20300);
#17804=AXIS2_PLACEMENT_3D('',#33461,#20301,#20302);
#17805=AXIS2_PLACEMENT_3D('',#33465,#20303,#20304);
#17806=AXIS2_PLACEMENT_3D('',#33469,#20305,#20306);
#17807=AXIS2_PLACEMENT_3D('',#33471,#20307,#20308);
#17808=AXIS2_PLACEMENT_3D('',#33486,#20310,#20311);
#17809=AXIS2_PLACEMENT_3D('',#33488,#20312,#20313);
#17810=AXIS2_PLACEMENT_3D('',#33491,#20315,#20316);
#17811=AXIS2_PLACEMENT_3D('',#33492,#20317,#20318);
#17812=AXIS2_PLACEMENT_3D('',#33495,#20320,#20321);
#17813=AXIS2_PLACEMENT_3D('',#33496,#20322,#20323);
#17814=AXIS2_PLACEMENT_3D('',#33498,#20325,#20326);
#17815=AXIS2_PLACEMENT_3D('',#33499,#20327,#20328);
#17816=AXIS2_PLACEMENT_3D('',#33500,#20329,#20330);
#17817=AXIS2_PLACEMENT_3D('',#33501,#20331,#20332);
#20222=DIRECTION('axis',(0.,0.,1.));
#20223=DIRECTION('refdir',(1.,0.,0.));
#20224=DIRECTION('center_axis',(-1.,0.,-2.84206292975234E-15));
#20225=DIRECTION('ref_axis',(0.,1.,3.18972570729564E-17));
#20226=DIRECTION('center_axis',(-1.,0.,0.));
#20227=DIRECTION('ref_axis',(0.,1.,0.));
#20228=DIRECTION('',(-0.25906346438713,-0.965860301192537,-8.85366735539473E-16));
#20229=DIRECTION('center_axis',(1.,0.,0.));
#20230=DIRECTION('ref_axis',(0.,1.,6.12323399573677E-17));
#20231=DIRECTION('center_axis',(1.,0.,0.));
#20232=DIRECTION('ref_axis',(0.,1.,6.12323399573677E-17));
#20233=DIRECTION('center_axis',(1.,0.,0.));
#20234=DIRECTION('ref_axis',(0.,1.,6.12323399573677E-17));
#20235=DIRECTION('center_axis',(1.,0.,0.));
#20236=DIRECTION('ref_axis',(0.,1.,6.12323399573677E-17));
#20237=DIRECTION('center_axis',(1.,0.,0.));
#20238=DIRECTION('ref_axis',(0.,1.,6.12323399573677E-17));
#20239=DIRECTION('center_axis',(1.,0.,0.));
#20240=DIRECTION('ref_axis',(0.,1.,6.12323399573677E-17));
#20241=DIRECTION('center_axis',(-1.,0.,0.));
#20242=DIRECTION('ref_axis',(0.,1.,0.));
#20243=DIRECTION('center_axis',(-1.,0.,0.));
#20244=DIRECTION('ref_axis',(0.,1.,0.));
#20245=DIRECTION('center_axis',(-1.,0.,0.));
#20246=DIRECTION('ref_axis',(0.,1.,0.));
#20247=DIRECTION('center_axis',(-1.,0.,0.));
#20248=DIRECTION('ref_axis',(0.,1.,0.));
#20249=DIRECTION('center_axis',(-1.,0.,0.));
#20250=DIRECTION('ref_axis',(0.,1.,0.));
#20251=DIRECTION('center_axis',(-1.,0.,0.));
#20252=DIRECTION('ref_axis',(0.,1.,0.));
#20253=DIRECTION('center_axis',(1.,0.,0.));
#20254=DIRECTION('ref_axis',(0.,0.,-1.));
#20255=DIRECTION('center_axis',(-1.,0.,0.));
#20256=DIRECTION('ref_axis',(0.,1.,0.));
#20257=DIRECTION('center_axis',(0.369289098563654,0.804810021844156,-0.464657282759296));
#20258=DIRECTION('ref_axis',(-0.782867463262138,0.,-0.622188504366245));
#20259=DIRECTION('',(-1.31968027496911E-14,-0.499999999999999,-0.866025403784439));
#20260=DIRECTION('center_axis',(0.36928909856366,-9.22265434949625E-13,
-0.929314565516994));
#20261=DIRECTION('ref_axis',(-0.929314565516994,0.,-0.36928909856366));
#20262=DIRECTION('',(-1.13115452140209E-14,-1.,-1.88525753567016E-15));
#20263=DIRECTION('center_axis',(0.369289098563657,0.804810021845078,0.464657282757696));
#20264=DIRECTION('ref_axis',(0.782867463261092,0.,-0.622188504367561));
#20265=DIRECTION('',(-1.31968027496911E-14,0.500000000000001,-0.866025403784438));
#20266=DIRECTION('center_axis',(0.369289098563656,-0.804810021845079,-0.464657282757697));
#20267=DIRECTION('ref_axis',(-0.782867463261094,0.,-0.622188504367559));
#20268=DIRECTION('',(-1.31968027496911E-14,-0.499999999999999,0.866025403784439));
#20269=DIRECTION('center_axis',(0.369289098563656,9.24740123922532E-13,
0.929314565516996));
#20270=DIRECTION('ref_axis',(0.929314565516995,0.,-0.369289098563656));
#20271=DIRECTION('',(-1.50820602853613E-14,1.,1.88525753567016E-15));
#20272=DIRECTION('center_axis',(0.369289098563655,-0.804810021844154,0.4646572827593));
#20273=DIRECTION('ref_axis',(0.78286746326214,0.,-0.622188504366242));
#20274=DIRECTION('',(-2.07378328923717E-14,0.500000000000004,0.866025403784436));
#20275=DIRECTION('center_axis',(0.,-0.866025403784437,0.500000000000004));
#20276=DIRECTION('ref_axis',(1.,0.,0.));
#20277=DIRECTION('',(1.,0.,0.));
#20278=DIRECTION('',(-1.,0.,0.));
#20279=DIRECTION('center_axis',(0.,-1.88525753567016E-15,1.));
#20280=DIRECTION('ref_axis',(1.,0.,0.));
#20281=DIRECTION('',(1.,0.,0.));
#20282=DIRECTION('',(-1.,0.,0.));
#20283=DIRECTION('center_axis',(0.,-0.866025403784439,-0.499999999999999));
#20284=DIRECTION('ref_axis',(0.,0.499999999999999,-0.866025403784439));
#20285=DIRECTION('',(1.,0.,0.));
#20286=DIRECTION('',(-1.,0.,0.));
#20287=DIRECTION('center_axis',(0.,0.866025403784438,0.500000000000001));
#20288=DIRECTION('ref_axis',(1.,0.,0.));
#20289=DIRECTION('',(1.,0.,0.));
#20290=DIRECTION('',(-1.,0.,0.));
#20291=DIRECTION('center_axis',(0.,1.88525753567016E-15,-1.));
#20292=DIRECTION('ref_axis',(-1.,0.,0.));
#20293=DIRECTION('',(1.,0.,0.));
#20294=DIRECTION('',(-1.,0.,0.));
#20295=DIRECTION('center_axis',(0.,0.866025403784439,-0.499999999999999));
#20296=DIRECTION('ref_axis',(0.,0.499999999999999,0.866025403784439));
#20297=DIRECTION('',(1.,0.,0.));
#20298=DIRECTION('',(-1.,0.,0.));
#20299=DIRECTION('center_axis',(0.,0.5,0.866025403784439));
#20300=DIRECTION('ref_axis',(0.,-0.866025403784439,0.5));
#20301=DIRECTION('center_axis',(0.,1.,-3.60555503696918E-16));
#20302=DIRECTION('ref_axis',(0.,3.60555503696918E-16,1.));
#20303=DIRECTION('center_axis',(0.,0.5,-0.866025403784439));
#20304=DIRECTION('ref_axis',(0.,0.866025403784439,0.5));
#20305=DIRECTION('center_axis',(1.,0.,0.));
#20306=DIRECTION('ref_axis',(0.,1.,0.));
#20307=DIRECTION('center_axis',(-1.,0.,0.));
#20308=DIRECTION('ref_axis',(0.,1.,0.));
#20309=DIRECTION('',(0.500438231481872,-0.865772242839476,-1.06026520598399E-16));
#20310=DIRECTION('center_axis',(-1.,0.,0.));
#20311=DIRECTION('ref_axis',(0.,1.,0.));
#20312=DIRECTION('center_axis',(1.,0.,0.));
#20313=DIRECTION('ref_axis',(0.,1.,0.));
#20314=DIRECTION('',(0.78086880944303,0.624695047554425,7.6503079043073E-17));
#20315=DIRECTION('center_axis',(1.,0.,0.));
#20316=DIRECTION('ref_axis',(0.,0.,-1.));
#20317=DIRECTION('center_axis',(1.,0.,0.));
#20318=DIRECTION('ref_axis',(0.,1.,0.));
#20319=DIRECTION('',(1.,0.,0.));
#20320=DIRECTION('center_axis',(1.,0.,0.));
#20321=DIRECTION('ref_axis',(0.,0.,-1.));
#20322=DIRECTION('center_axis',(1.,0.,0.));
#20323=DIRECTION('ref_axis',(0.,1.,0.));
#20324=DIRECTION('',(0.780868809443029,-0.624695047554425,-7.6503079043073E-17));
#20325=DIRECTION('center_axis',(0.,-0.5,-0.866025403784439));
#20326=DIRECTION('ref_axis',(0.,0.866025403784439,-0.5));
#20327=DIRECTION('center_axis',(0.,-1.,-1.20185167898973E-16));
#20328=DIRECTION('ref_axis',(0.,1.20185167898973E-16,-1.));
#20329=DIRECTION('center_axis',(0.,-0.5,0.866025403784439));
#20330=DIRECTION('ref_axis',(0.,-0.866025403784439,-0.5));
#20331=DIRECTION('center_axis',(1.,0.,0.));
#20332=DIRECTION('ref_axis',(0.,0.,-1.));
#32886=CARTESIAN_POINT('',(0.,0.,0.));
#32887=CARTESIAN_POINT('Origin',(8.31492550064808,0.,-2.41787080875326E-16));
#32888=CARTESIAN_POINT('',(8.4,-7.26300281800529,8.89461315326838E-16));
#32889=CARTESIAN_POINT('Origin',(8.4,0.,0.));
#32890=CARTESIAN_POINT('',(8.27136742382219,-7.74615915544327,-0.000941532553519379));
#32891=CARTESIAN_POINT('',(8.31492550064808,-7.580184099288,-1.41187898116472E-15));
#32892=CARTESIAN_POINT('',(8.23004515173475,-7.70339232440972,-1.73638161370287));
#32893=CARTESIAN_POINT('Ctrl Pts',(8.27136742382219,-7.74615915544327,-0.000941532553519405));
#32894=CARTESIAN_POINT('Ctrl Pts',(8.27114725188007,-7.74616681794042,-0.064564222478092));
#32895=CARTESIAN_POINT('Ctrl Pts',(8.27077282593737,-7.74599899203376,-0.128189559455883));
#32896=CARTESIAN_POINT('Ctrl Pts',(8.27025171390506,-7.7456553806079,-0.191831784430464));
#32897=CARTESIAN_POINT('Ctrl Pts',(8.26916283644786,-7.74493739539079,-0.324813906898557));
#32898=CARTESIAN_POINT('Ctrl Pts',(8.26743494441316,-7.74345241079881,-0.457721426103084));
#32899=CARTESIAN_POINT('Ctrl Pts',(8.26514537190407,-7.741203690555,-0.590678771338576));
#32900=CARTESIAN_POINT('Ctrl Pts',(8.26401462256671,-7.74009311689312,-0.656342308712543));
#32901=CARTESIAN_POINT('Ctrl Pts',(8.26274700585539,-7.73879620770269,-0.722017728961687));
#32902=CARTESIAN_POINT('Ctrl Pts',(8.2613337016924,-7.73731374873599,-0.787718335582255));
#32903=CARTESIAN_POINT('Ctrl Pts',(8.25841332256419,-7.73425047167353,-0.923478694398744));
#32904=CARTESIAN_POINT('Ctrl Pts',(8.25487528348693,-7.73039901514795,-1.05914211268319));
#32905=CARTESIAN_POINT('Ctrl Pts',(8.25065191470568,-7.72577657208149,-1.19484477917841));
#32906=CARTESIAN_POINT('Ctrl Pts',(8.2466296968618,-7.72137428709354,-1.32408418850076));
#32907=CARTESIAN_POINT('Ctrl Pts',(8.24198575526578,-7.71627263760997,-1.45335936506934));
#32908=CARTESIAN_POINT('Ctrl Pts',(8.23668284834012,-7.7104847667795,-1.58274529764113));
#32909=CARTESIAN_POINT('Ctrl Pts',(8.23461699541548,-7.7082299865146,-1.63315016254979));
#32910=CARTESIAN_POINT('Ctrl Pts',(8.23245137951942,-7.7058710484806,-1.68357135020396));
#32911=CARTESIAN_POINT('Ctrl Pts',(8.23018478415278,-7.7034086872879,-1.73401135130111));
#32912=CARTESIAN_POINT('',(8.23406708607797,-5.35358430006243,-5.80403694227773));
#32913=CARTESIAN_POINT('Origin',(8.22985100129616,0.,-4.83574161750652E-16));
#32914=CARTESIAN_POINT('',(8.23005205545796,-2.349628256023,-7.53857080762849));
#32915=CARTESIAN_POINT('Ctrl Pts',(8.23529955888936,-5.35220883424223,-5.80478584085023));
#32916=CARTESIAN_POINT('Ctrl Pts',(8.24135251359355,-5.24157560348415,-5.87606344132463));
#32917=CARTESIAN_POINT('Ctrl Pts',(8.24663904490831,-5.13069470185511,-5.94667945173788));
#32918=CARTESIAN_POINT('Ctrl Pts',(8.25115307889962,-5.01950382509813,-6.01665379089667));
#32919=CARTESIAN_POINT('Ctrl Pts',(8.25514467229576,-4.92118184297989,-6.07852951239622));
#32920=CARTESIAN_POINT('Ctrl Pts',(8.25853265795554,-4.82261664919146,-6.13990399257126));
#32921=CARTESIAN_POINT('Ctrl Pts',(8.26132675188252,-4.72373802018084,-6.20080573283235));
#32922=CARTESIAN_POINT('Ctrl Pts',(8.26482295844291,-4.60001271943482,-6.27701113945212));
#32923=CARTESIAN_POINT('Ctrl Pts',(8.2673830227026,-4.47597208224258,-6.3523685972828));
#32924=CARTESIAN_POINT('Ctrl Pts',(8.26904864667115,-4.35149112259367,-6.42693880010717));
#32925=CARTESIAN_POINT('Ctrl Pts',(8.26988529460047,-4.28896396214428,-6.46439563728045));
#32926=CARTESIAN_POINT('Ctrl Pts',(8.27049679382362,-4.22632502082287,-6.50165417994343));
#32927=CARTESIAN_POINT('Ctrl Pts',(8.2708913591938,-4.16355502052887,-6.53872370512012));
#32928=CARTESIAN_POINT('Ctrl Pts',(8.27184482310895,-4.01187184010239,-6.62830190249728));
#32929=CARTESIAN_POINT('Ctrl Pts',(8.27152555460945,-3.85965879652205,-6.71663856576674));
#32930=CARTESIAN_POINT('Ctrl Pts',(8.27008277805002,-3.70666429170934,-6.80387205524455));
#32931=CARTESIAN_POINT('Ctrl Pts',(8.26899334829348,-3.59113928886561,-6.86974140873753));
#32932=CARTESIAN_POINT('Ctrl Pts',(8.26726627003468,-3.47529564565701,-6.93490905860148));
#32933=CARTESIAN_POINT('Ctrl Pts',(8.264979096865,-3.35902727876003,-6.99944001442568));
#32934=CARTESIAN_POINT('Ctrl Pts',(8.26384953248748,-3.30160591372285,-7.03130986578313));
#32935=CARTESIAN_POINT('Ctrl Pts',(8.26258348671553,-3.24408116185127,-7.0630242403131));
#32936=CARTESIAN_POINT('Ctrl Pts',(8.26117208730693,-3.18644188536852,-7.09459047623395));
#32937=CARTESIAN_POINT('Ctrl Pts',(8.25825582835368,-3.06734657111715,-7.1598132030989));
#32938=CARTESIAN_POINT('Ctrl Pts',(8.25472340542738,-2.94794142432279,-7.22430479440537));
#32939=CARTESIAN_POINT('Ctrl Pts',(8.25050669481373,-2.82811703428188,-7.28814827091774));
#32940=CARTESIAN_POINT('Ctrl Pts',(8.24649089566865,-2.71400185608383,-7.34894982973649));
#32941=CARTESIAN_POINT('Ctrl Pts',(8.24185434137902,-2.59950625281144,-7.4091635865651));
#32942=CARTESIAN_POINT('Ctrl Pts',(8.23655941543651,-2.48457179585488,-7.46883845050572));
#32943=CARTESIAN_POINT('Ctrl Pts',(8.23449571308963,-2.43977598357458,-7.49209678463563));
#32944=CARTESIAN_POINT('Ctrl Pts',(8.23233224536128,-2.3949139212779,-7.51527300286226));
#32945=CARTESIAN_POINT('Ctrl Pts',(8.23006777285707,-2.34998381317915,-7.53836899137533));
#32946=CARTESIAN_POINT('',(8.23406708607796,2.3496512864847,-7.53835847629444));
#32947=CARTESIAN_POINT('Origin',(8.22985100129616,0.,-4.83574161750652E-16));
#32948=CARTESIAN_POINT('',(8.23005205545723,5.35377969962258,-5.80412316297992));
#32949=CARTESIAN_POINT('Ctrl Pts',(8.23529955888937,2.35098758458347,-7.53754173723834));
#32950=CARTESIAN_POINT('Ctrl Pts',(8.24135251359366,2.46803241269599,-7.47736934913535));
#32951=CARTESIAN_POINT('Ctrl Pts',(8.24663904490848,2.58462812244407,-7.41665167673576));
#32952=CARTESIAN_POINT('Ctrl Pts',(8.25115307889983,2.70082311614886,-7.35534472237359));
#32953=CARTESIAN_POINT('Ctrl Pts',(8.25514467229588,2.8035700539023,-7.30113324885945));
#32954=CARTESIAN_POINT('Ctrl Pts',(8.25853265795559,2.90600450977038,-7.24646052719819));
#32955=CARTESIAN_POINT('Ctrl Pts',(8.26132675188253,3.00818627847469,-7.19127999271513));
#32956=CARTESIAN_POINT('Ctrl Pts',(8.26482295844286,3.13604474688414,-7.12223344248917));
#32957=CARTESIAN_POINT('Ctrl Pts',(8.26738302270252,3.2633265383243,-7.05248982849551));
#32958=CARTESIAN_POINT('Ctrl Pts',(8.26904864667108,3.39014670815809,-6.98197125656537));
#32959=CARTESIAN_POINT('Ctrl Pts',(8.26988529460043,3.45384886092223,-6.94654956577526));
#32960=CARTESIAN_POINT('Ctrl Pts',(8.27049679382361,3.51743517603901,-6.91093192265516));
#32961=CARTESIAN_POINT('Ctrl Pts',(8.2708913591938,3.5809233266972,-6.87510627039224));
#32962=CARTESIAN_POINT('Ctrl Pts',(8.27184482310895,3.73434191146413,-6.78853388150475));
#32963=CARTESIAN_POINT('Ctrl Pts',(8.27152555460945,3.88695022773128,-6.70088185061152));
#32964=CARTESIAN_POINT('Ctrl Pts',(8.27008277805002,4.03899389808625,-6.61200146754316));
#32965=CARTESIAN_POINT('Ctrl Pts',(8.26899334829347,4.15380093296388,-6.54488855705472));
#32966=CARTESIAN_POINT('Ctrl Pts',(8.26726627003468,4.26815959485526,-6.47714884410112));
#32967=CARTESIAN_POINT('Ctrl Pts',(8.264979096865,4.38217922537795,-6.40872296262395));
#32968=CARTESIAN_POINT('Ctrl Pts',(8.26384953248747,4.43849000878697,-6.37492952746046));
#32969=CARTESIAN_POINT('Ctrl Pts',(8.26258348671552,4.49471783873088,-6.34096881825824));
#32970=CARTESIAN_POINT('Ctrl Pts',(8.26117208730692,4.5508746391816,-6.30683485852883));
#32971=CARTESIAN_POINT('Ctrl Pts',(8.25825582835373,4.66690683467426,-6.23630665434924));
#32972=CARTESIAN_POINT('Ctrl Pts',(8.2547234054275,4.78246076447121,-6.16514455953727));
#32973=CARTESIAN_POINT('Ctrl Pts',(8.25050669481395,4.89766303201517,-6.09329533202641));
#32974=CARTESIAN_POINT('Ctrl Pts',(8.2464908956689,5.0073763156408,-6.02486946815899));
#32975=CARTESIAN_POINT('Ctrl Pts',(8.24185434137931,5.11677076034776,-5.95582024551788));
#32976=CARTESIAN_POINT('Ctrl Pts',(8.23655941543682,5.22591793696589,-5.88612151799374));
#32977=CARTESIAN_POINT('Ctrl Pts',(8.23449571308984,5.26845815131449,-5.85895637363939));
#32978=CARTESIAN_POINT('Ctrl Pts',(8.23233224536139,5.31096037621297,-5.83169279713619));
#32979=CARTESIAN_POINT('Ctrl Pts',(8.23006777285706,5.35342714304242,-5.80433017638299));
#32980=CARTESIAN_POINT('',(8.23016251323912,7.70340607746227,-1.73438940040554));
#32981=CARTESIAN_POINT('Origin',(8.22985100129616,0.,-4.83574161750652E-16));
#32982=CARTESIAN_POINT('',(8.23416387505949,7.7032334399193,1.73431147348199));
#32983=CARTESIAN_POINT('Ctrl Pts',(8.23018478415278,7.70340868728788,-1.73401135130117));
#32984=CARTESIAN_POINT('Ctrl Pts',(8.23606248521678,7.70979404535193,-1.60321109798711));
#32985=CARTESIAN_POINT('Ctrl Pts',(8.24125906760293,7.71548549605284,-1.47252342627014));
#32986=CARTESIAN_POINT('Ctrl Pts',(8.24580484326341,7.72046864985948,-1.34188213816602));
#32987=CARTESIAN_POINT('Ctrl Pts',(8.24986158901183,7.72491572105892,-1.22529510667363));
#32988=CARTESIAN_POINT('Ctrl Pts',(8.25340050977611,7.72879871129239,-1.10874408188086));
#32989=CARTESIAN_POINT('Ctrl Pts',(8.25645834823089,7.73210645326191,-0.99215053002542));
#32990=CARTESIAN_POINT('Ctrl Pts',(8.25997021137989,7.7359053253413,-0.858245288062264));
#32991=CARTESIAN_POINT('Ctrl Pts',(8.26284235113813,7.73894065122346,-0.724458427579585));
#32992=CARTESIAN_POINT('Ctrl Pts',(8.26514559776231,7.74120355991351,-0.590678780796379));
#32993=CARTESIAN_POINT('Ctrl Pts',(8.26659397190069,7.74262656793607,-0.506552756858444));
#32994=CARTESIAN_POINT('Ctrl Pts',(8.26781796450162,7.74374408224676,-0.422428818173793));
#32995=CARTESIAN_POINT('Ctrl Pts',(8.26879776569929,7.74455470315058,-0.338274320859049));
#32996=CARTESIAN_POINT('Ctrl Pts',(8.27084831243718,7.74625118612486,-0.162154174894971));
#32997=CARTESIAN_POINT('Ctrl Pts',(8.27182204063112,7.74660194359562,0.0138274237015491));
#32998=CARTESIAN_POINT('Ctrl Pts',(8.27155825637708,7.74560977596245,0.189957727593904));
#32999=CARTESIAN_POINT('Ctrl Pts',(8.27133104131297,7.74475515545753,0.341670567454257));
#33000=CARTESIAN_POINT('Ctrl Pts',(8.27018653488307,7.74290486336108,0.493304050874034));
#33001=CARTESIAN_POINT('Ctrl Pts',(8.26805044484228,7.74006940953455,0.645040539895604));
#33002=CARTESIAN_POINT('Ctrl Pts',(8.26738920277765,7.73919167437049,0.692011663473354));
#33003=CARTESIAN_POINT('Ctrl Pts',(8.26663319490192,7.73821950084626,0.738992406975978));
#33004=CARTESIAN_POINT('Ctrl Pts',(8.26578093504743,7.73715311288952,0.785987382532037));
#33005=CARTESIAN_POINT('Ctrl Pts',(8.26331387784144,7.73406621388893,0.922024874477323));
#33006=CARTESIAN_POINT('Ctrl Pts',(8.26004379084571,7.73019397599313,1.05797667576818));
#33007=CARTESIAN_POINT('Ctrl Pts',(8.25594566859687,7.7255526051338,1.19397572905201));
#33008=CARTESIAN_POINT('Ctrl Pts',(8.25203090646028,7.72111890067145,1.32388984875875));
#33009=CARTESIAN_POINT('Ctrl Pts',(8.24736050788044,7.71598329279669,1.45384728169982));
#33010=CARTESIAN_POINT('Ctrl Pts',(8.24193338497957,7.71015840635703,1.58392070057521));
#33011=CARTESIAN_POINT('Ctrl Pts',(8.23986380764802,7.70793714600331,1.63352285701424));
#33012=CARTESIAN_POINT('Ctrl Pts',(8.23768441207748,7.70561563896657,1.68314140347541));
#33013=CARTESIAN_POINT('Ctrl Pts',(8.23539599829651,7.70319454879583,1.73277853165711));
#33014=CARTESIAN_POINT('',(8.23406708607805,5.35358430006271,5.80403694227756));
#33015=CARTESIAN_POINT('Origin',(8.22985100129616,0.,-4.83574161750652E-16));
#33016=CARTESIAN_POINT('',(8.23005205545717,2.34962825602276,7.53857080762868));
#33017=CARTESIAN_POINT('Ctrl Pts',(8.23529955888929,5.35220883424264,5.80478584084999));
#33018=CARTESIAN_POINT('Ctrl Pts',(8.24135251359347,5.24157560348494,5.87606344132415));
#33019=CARTESIAN_POINT('Ctrl Pts',(8.24663904490822,5.13069470185628,5.94667945173717));
#33020=CARTESIAN_POINT('Ctrl Pts',(8.25115307889952,5.01950382509967,6.01665379089573));
#33021=CARTESIAN_POINT('Ctrl Pts',(8.25514467229569,4.92118184298078,6.07852951239569));
#33022=CARTESIAN_POINT('Ctrl Pts',(8.25853265795549,4.8226166491917,6.13990399257113));
#33023=CARTESIAN_POINT('Ctrl Pts',(8.26132675188249,4.72373802018044,6.20080573283262));
#33024=CARTESIAN_POINT('Ctrl Pts',(8.26482295844295,4.60001271943165,6.27701113945411));
#33025=CARTESIAN_POINT('Ctrl Pts',(8.26738302270268,4.47597208223666,6.35236859728643));
#33026=CARTESIAN_POINT('Ctrl Pts',(8.26904864667122,4.35149112258499,6.4269388001124));
#33027=CARTESIAN_POINT('Ctrl Pts',(8.26988529460048,4.28896396213838,6.46439563728399));
#33028=CARTESIAN_POINT('Ctrl Pts',(8.2704967938236,4.22632502081977,6.50165417994529));
#33029=CARTESIAN_POINT('Ctrl Pts',(8.27089135919375,4.16355502052857,6.53872370512033));
#33030=CARTESIAN_POINT('Ctrl Pts',(8.2718448231089,4.01187184010217,6.62830190249743));
#33031=CARTESIAN_POINT('Ctrl Pts',(8.2715255546094,3.8596587965218,6.71663856576692));
#33032=CARTESIAN_POINT('Ctrl Pts',(8.27008277804997,3.70666429170905,6.80387205524474));
#33033=CARTESIAN_POINT('Ctrl Pts',(8.26899334829342,3.59113928886542,6.86974140873767));
#33034=CARTESIAN_POINT('Ctrl Pts',(8.26726627003463,3.47529564565692,6.93490905860157));
#33035=CARTESIAN_POINT('Ctrl Pts',(8.26497909686495,3.35902727876005,6.99944001442571));
#33036=CARTESIAN_POINT('Ctrl Pts',(8.26384953248743,3.30160591372274,7.03130986578322));
#33037=CARTESIAN_POINT('Ctrl Pts',(8.26258348671547,3.24408116185103,7.06302424031326));
#33038=CARTESIAN_POINT('Ctrl Pts',(8.26117208730687,3.18644188536816,7.09459047623419));
#33039=CARTESIAN_POINT('Ctrl Pts',(8.25825582835368,3.06734657111932,7.15981320309774));
#33040=CARTESIAN_POINT('Ctrl Pts',(8.25472340542746,2.9479414243275,7.22430479440286));
#33041=CARTESIAN_POINT('Ctrl Pts',(8.25050669481393,2.82811703428916,7.2881482709139));
#33042=CARTESIAN_POINT('Ctrl Pts',(8.24649089566889,2.71400185609146,7.34894982973249));
#33043=CARTESIAN_POINT('Ctrl Pts',(8.24185434137931,2.59950625281942,7.40916358656095));
#33044=CARTESIAN_POINT('Ctrl Pts',(8.23655941543684,2.48457179586321,7.46883845050143));
#33045=CARTESIAN_POINT('Ctrl Pts',(8.23449571308983,2.43977598357996,7.49209678463289));
#33046=CARTESIAN_POINT('Ctrl Pts',(8.23233224536135,2.3949139212803,7.51527300286106));
#33047=CARTESIAN_POINT('Ctrl Pts',(8.23006777285699,2.34998381317858,7.53836899137566));
#33048=CARTESIAN_POINT('',(8.23005205545787,-2.34962825602266,7.53857080762868));
#33049=CARTESIAN_POINT('Origin',(8.22985100129616,0.,-4.83574161750652E-16));
#33050=CARTESIAN_POINT('',(8.23406708607805,-5.35358430006267,5.8040369422776));
#33051=CARTESIAN_POINT('Ctrl Pts',(8.23006777285699,-2.34998381317852,7.53836899137568));
#33052=CARTESIAN_POINT('Ctrl Pts',(8.23593724524199,-2.46644185285449,7.47850460064909));
#33053=CARTESIAN_POINT('Ctrl Pts',(8.24112605624522,-2.58245558527781,7.41809559395111));
#33054=CARTESIAN_POINT('Ctrl Pts',(8.24566489205474,-2.69807519938032,7.35709638054601));
#33055=CARTESIAN_POINT('Ctrl Pts',(8.24971614773269,-2.80127448610756,7.30264994978083));
#33056=CARTESIAN_POINT('Ctrl Pts',(8.25325006140408,-2.90416059898131,7.24773285475222));
#33057=CARTESIAN_POINT('Ctrl Pts',(8.25630367580332,-3.00679603469776,7.19229611263911));
#33058=CARTESIAN_POINT('Ctrl Pts',(8.2598103660455,-3.12465986223869,7.12863402004664));
#33059=CARTESIAN_POINT('Ctrl Pts',(8.26267849028981,-3.24203961276667,7.06436972340848));
#33060=CARTESIAN_POINT('Ctrl Pts',(8.26497932272721,-3.35902720524777,6.99943990601788));
#33061=CARTESIAN_POINT('Ctrl Pts',(8.26642617872781,-3.43259370988549,6.95860942467462));
#33062=CARTESIAN_POINT('Ctrl Pts',(8.26764928689471,-3.5060057796466,6.9175153435751));
#33063=CARTESIAN_POINT('Ctrl Pts',(8.26862878428063,-3.57929097436323,6.87614013651681));
#33064=CARTESIAN_POINT('Ctrl Pts',(8.27067869519549,-3.73266363538966,6.78954930965762));
#33065=CARTESIAN_POINT('Ctrl Pts',(8.27165433670821,-3.88524391789899,6.70186202116604));
#33066=CARTESIAN_POINT('Ctrl Pts',(8.27139442937721,-4.03728187947163,6.61293714414642));
#33067=CARTESIAN_POINT('Ctrl Pts',(8.27117054495976,-4.16824752143661,6.5363371721061));
#33068=CARTESIAN_POINT('Ctrl Pts',(8.27003074605399,-4.29864682375577,6.45891436751854));
#33069=CARTESIAN_POINT('Ctrl Pts',(8.26790031375505,-4.42864291466266,6.38058668870114));
#33070=CARTESIAN_POINT('Ctrl Pts',(8.26724093283417,-4.46887744461066,6.35634382634158));
#33071=CARTESIAN_POINT('Ctrl Pts',(8.2664869086185,-4.5090731150744,6.33201437801959));
#33072=CARTESIAN_POINT('Ctrl Pts',(8.26563674296381,-4.54923402841569,6.30759623376819));
#33073=CARTESIAN_POINT('Ctrl Pts',(8.2631754786934,-4.66550151173327,6.23690470951749));
#33074=CARTESIAN_POINT('Ctrl Pts',(8.25991192457676,-4.78130226349205,6.16557584420391));
#33075=CARTESIAN_POINT('Ctrl Pts',(8.25582077331136,-4.89675945875543,6.093557235874));
#33076=CARTESIAN_POINT('Ctrl Pts',(8.2519127078451,-5.00704975319055,6.02476157961894));
#33077=CARTESIAN_POINT('Ctrl Pts',(8.24724941988421,-5.11702669300951,5.95533638684039));
#33078=CARTESIAN_POINT('Ctrl Pts',(8.24182957345511,-5.22675947892738,5.88525628231459));
#33079=CARTESIAN_POINT('Ctrl Pts',(8.23976246583453,-5.26861112195184,5.85852801242517));
#33080=CARTESIAN_POINT('Ctrl Pts',(8.23758553184529,-5.31042683092239,5.83170470527504));
#33081=CARTESIAN_POINT('Ctrl Pts',(8.23529955888929,-5.3522088342426,5.80478584085003));
#33082=CARTESIAN_POINT('',(8.23416387505187,-7.70323343991956,1.73431147348703));
#33083=CARTESIAN_POINT('Origin',(8.22985100129616,0.,-4.83574161750652E-16));
#33084=CARTESIAN_POINT('Ctrl Pts',(8.23539599829651,-7.70319454879582,1.73277853165718));
#33085=CARTESIAN_POINT('Ctrl Pts',(8.24145629544956,-7.7096062065087,1.6013268907403));
#33086=CARTESIAN_POINT('Ctrl Pts',(8.24675009530479,-7.71532104571645,1.46999154471252));
#33087=CARTESIAN_POINT('Ctrl Pts',(8.25127107718454,-7.72032516451686,1.33870852056237));
#33088=CARTESIAN_POINT('Ctrl Pts',(8.25526860263604,-7.72474988746401,1.2226259428503));
#33089=CARTESIAN_POINT('Ctrl Pts',(8.25866233313259,-7.72861895281961,1.10658330096045));
#33090=CARTESIAN_POINT('Ctrl Pts',(8.26146180005289,-7.73192193321259,0.990505496974222));
#33091=CARTESIAN_POINT('Ctrl Pts',(8.26496480270566,-7.73605498761474,0.84525610954886));
#33092=CARTESIAN_POINT('Ctrl Pts',(8.26753103166903,-7.73929605042608,0.700157460155893));
#33093=CARTESIAN_POINT('Ctrl Pts',(8.26920181683445,-7.74163519278412,0.555070887179658));
#33094=CARTESIAN_POINT('Ctrl Pts',(8.27004107552342,-7.74281017661169,0.482191878230534));
#33095=CARTESIAN_POINT('Ctrl Pts',(8.27065492237978,-7.74375753797758,0.40931515587787));
#33096=CARTESIAN_POINT('Ctrl Pts',(8.27105152573793,-7.74447567221088,0.336419375462664));
#33097=CARTESIAN_POINT('Ctrl Pts',(8.27166357551873,-7.74558391774399,0.223924497373578));
#33098=CARTESIAN_POINT('Ctrl Pts',(8.27175674710727,-7.74614548493137,0.111495968856029));
#33099=CARTESIAN_POINT('Ctrl Pts',(8.27136742382219,-7.74615915544327,-0.000941532553519405));
#33100=CARTESIAN_POINT('Ctrl Pts',(7.18908433792779,0.266497816746017,9.08374172079725));
#33101=CARTESIAN_POINT('Ctrl Pts',(7.58326629775444,1.49147728388782,8.37649949569117));
#33102=CARTESIAN_POINT('Ctrl Pts',(8.01233031911798,3.87343953744646,7.00127294739956));
#33103=CARTESIAN_POINT('Ctrl Pts',(7.71466028436332,6.10019622706514,5.71565437322842));
#33104=CARTESIAN_POINT('Ctrl Pts',(7.1890843379278,7.73350218325398,4.77266473975377));
#33105=CARTESIAN_POINT('Ctrl Pts',(7.34585286708095,0.177665211164012,9.01725418637031));
#33106=CARTESIAN_POINT('Ctrl Pts',(7.74659985034045,1.41147052678102,8.3070863945685));
#33107=CARTESIAN_POINT('Ctrl Pts',(8.18799973158063,3.82236863432499,6.91940076517965));
#33108=CARTESIAN_POINT('Ctrl Pts',(7.88018217809361,6.07777058358531,5.61372014708539));
#33109=CARTESIAN_POINT('Ctrl Pts',(7.34585286708095,7.72033859219626,4.66248967942191));
#33110=CARTESIAN_POINT('Ctrl Pts',(7.5026213962341,0.0888326055820073,8.95076665194336));
#33111=CARTESIAN_POINT('Ctrl Pts',(7.90993340292647,1.33146376967423,8.23767329344583));
#33112=CARTESIAN_POINT('Ctrl Pts',(8.36366914404328,3.77129773120352,6.83752858295973));
#33113=CARTESIAN_POINT('Ctrl Pts',(8.04570407182389,6.05534494010548,5.51178592094237));
#33114=CARTESIAN_POINT('Ctrl Pts',(7.5026213962341,7.70717500113854,4.55231461909006));
#33115=CARTESIAN_POINT('Ctrl Pts',(7.65938992538726,2.4980018054066E-15,
8.88427911751642));
#33116=CARTESIAN_POINT('Ctrl Pts',(8.07326695551249,1.25145701256744,8.16826019232316));
#33117=CARTESIAN_POINT('Ctrl Pts',(8.53933855650593,3.72022682808205,6.75565640073981));
#33118=CARTESIAN_POINT('Ctrl Pts',(8.21122596555418,6.03291929662566,5.40985169479934));
#33119=CARTESIAN_POINT('Ctrl Pts',(7.65938992538726,7.69401141008081,4.4421395587582));
#33120=CARTESIAN_POINT('',(7.65938992538726,7.69401141008081,4.4421395587582));
#33121=CARTESIAN_POINT('Ctrl Pts',(8.2352995588869,5.35220883425915,5.8047858408404));
#33122=CARTESIAN_POINT('Ctrl Pts',(8.12981699914252,6.07857291110272,5.38302716017364));
#33123=CARTESIAN_POINT('Ctrl Pts',(7.94257793183433,6.84158182974382,4.93874443896362));
#33124=CARTESIAN_POINT('Ctrl Pts',(7.65938992538726,7.69401141008081,4.4421395587582));
#33125=CARTESIAN_POINT('',(7.1980528062909,7.70555136271414,4.78880215351652));
#33126=CARTESIAN_POINT('Ctrl Pts',(7.1980528062909,7.70555136271414,4.78880215351652));
#33127=CARTESIAN_POINT('Ctrl Pts',(7.27501095230305,7.70355337375233,4.73109983436028));
#33128=CARTESIAN_POINT('Ctrl Pts',(7.35194075983994,7.70159253788117,4.67335568633266));
#33129=CARTESIAN_POINT('Ctrl Pts',(7.5057189835248,7.69774589003655,4.55780213135815));
#33130=CARTESIAN_POINT('Ctrl Pts',(7.58257003626918,7.69585999385014,4.49999077482194));
#33131=CARTESIAN_POINT('Ctrl Pts',(7.65938992538726,7.69401141008081,4.4421395587582));
#33132=CARTESIAN_POINT('',(7.19805280629065,0.29444863728671,9.06760430703401));
#33133=CARTESIAN_POINT('Ctrl Pts',(7.19805611451105,7.70554822452627,4.78880396535013));
#33134=CARTESIAN_POINT('Ctrl Pts',(7.71659579227932,6.08565785082646,5.7240481086634));
#33135=CARTESIAN_POINT('Ctrl Pts',(8.009965927807,3.87293458424719,7.00156448226508));
#33136=CARTESIAN_POINT('Ctrl Pts',(7.58605957246042,1.50702556652582,8.36752269052469));
#33137=CARTESIAN_POINT('Ctrl Pts',(7.19805432694391,0.294451576737634,9.06760260994123));
#33138=CARTESIAN_POINT('',(7.65938992538726,2.51671144589255E-15,8.88427911751642));
#33139=CARTESIAN_POINT('Ctrl Pts',(7.65938992538726,2.51671144589255E-15,
8.88427911751642));
#33140=CARTESIAN_POINT('Ctrl Pts',(7.58256899052649,0.04917700029988,8.91480606160851));
#33141=CARTESIAN_POINT('Ctrl Pts',(7.50571689117296,0.0983008235915428,
8.94534538978223));
#33142=CARTESIAN_POINT('Ctrl Pts',(7.35193866587405,0.196449810832569,9.00645346266353));
#33143=CARTESIAN_POINT('Ctrl Pts',(7.27500990494312,0.245476624013931,9.03702325445621));
#33144=CARTESIAN_POINT('Ctrl Pts',(7.1980528062913,0.294448637287157,9.06760430703376));
#33145=CARTESIAN_POINT('Ctrl Pts',(7.65938992538726,2.4980018054066E-15,
8.88427911751642));
#33146=CARTESIAN_POINT('Ctrl Pts',(7.94257793183434,0.856287232069759,8.39435588610997));
#33147=CARTESIAN_POINT('Ctrl Pts',(8.12551492847749,1.62202366451198,7.95622077152865));
#33148=CARTESIAN_POINT('Ctrl Pts',(8.23006777285462,2.34998381316211,7.53836899138512));
#33149=CARTESIAN_POINT('Ctrl Pts',(7.18908433792779,8.,4.31107698104349));
#33150=CARTESIAN_POINT('Ctrl Pts',(7.71466028436332,8.,2.42509771409394));
#33151=CARTESIAN_POINT('Ctrl Pts',(8.01268601649393,8.,-0.14606847802148));
#33152=CARTESIAN_POINT('Ctrl Pts',(7.58326629775444,8.,-2.89659253083151));
#33153=CARTESIAN_POINT('Ctrl Pts',(7.1890843379278,8.,-4.31107698104348));
#33154=CARTESIAN_POINT('Ctrl Pts',(7.34585286708095,7.89800380336027,4.35476450694839));
#33155=CARTESIAN_POINT('Ctrl Pts',(7.88018217809362,7.90050954890513,2.45664365021571));
#33156=CARTESIAN_POINT('Ctrl Pts',(8.18834927452041,7.90355897903611,-0.149358354443887));
#33157=CARTESIAN_POINT('Ctrl Pts',(7.74659985034045,7.89988311251891,-2.93117386439906));
#33158=CARTESIAN_POINT('Ctrl Pts',(7.34585286708095,7.89800380336027,-4.35476450694839));
#33159=CARTESIAN_POINT('Ctrl Pts',(7.5026213962341,7.79600760672054,4.3984520328533));
#33160=CARTESIAN_POINT('Ctrl Pts',(8.04570407182393,7.80101909781026,2.48818958633749));
#33161=CARTESIAN_POINT('Ctrl Pts',(8.36401253254689,7.80711795807222,-0.152648230866291));
#33162=CARTESIAN_POINT('Ctrl Pts',(7.90993340292645,7.79976622503781,-2.96575519796661));
#33163=CARTESIAN_POINT('Ctrl Pts',(7.50262139623411,7.79600760672054,-4.3984520328533));
#33164=CARTESIAN_POINT('Ctrl Pts',(7.65938992538726,7.69401141008081,4.44213955875821));
#33165=CARTESIAN_POINT('Ctrl Pts',(8.21122596555423,7.70152864671539,2.51973552245926));
#33166=CARTESIAN_POINT('Ctrl Pts',(8.53967579057337,7.71067693710833,-0.155938107288697));
#33167=CARTESIAN_POINT('Ctrl Pts',(8.07326695551245,7.69964933755672,-3.00033653153417));
#33168=CARTESIAN_POINT('Ctrl Pts',(7.65938992538726,7.69401141008081,-4.44213955875822));
#33169=CARTESIAN_POINT('',(7.65938992538726,7.69401141008081,-4.44213955875821));
#33170=CARTESIAN_POINT('Ctrl Pts',(8.23018478415036,7.70340868728783,-1.73401135132057));
#33171=CARTESIAN_POINT('Ctrl Pts',(8.12558259310879,7.7012998264511,-2.57338080520911));
#33172=CARTESIAN_POINT('Ctrl Pts',(7.94257793183433,7.69786906181353,-3.45561144714637));
#33173=CARTESIAN_POINT('Ctrl Pts',(7.65938992538726,7.69401141008081,-4.44213955875822));
#33174=CARTESIAN_POINT('',(7.1980528062909,8.,-4.27880215351799));
#33175=CARTESIAN_POINT('Ctrl Pts',(7.1980528062909,8.,-4.27880215351799));
#33176=CARTESIAN_POINT('Ctrl Pts',(7.27501095230391,7.94902933127194,-4.305923003899));
#33177=CARTESIAN_POINT('Ctrl Pts',(7.35194075984025,7.89804101422492,-4.33309694423554));
#33178=CARTESIAN_POINT('Ctrl Pts',(7.50571898351011,7.79604537620704,-4.38754242696464));
#33179=CARTESIAN_POINT('Ctrl Pts',(7.58257003626179,7.7450363247214,-4.41481487122897));
#33180=CARTESIAN_POINT('Ctrl Pts',(7.65938992538726,7.69401141008081,-4.44213955875821));
#33181=CARTESIAN_POINT('',(7.19805280629065,8.,4.27880215351701));
#33182=CARTESIAN_POINT('Ctrl Pts',(7.19805435334672,8.,-4.27879875406529));
#33183=CARTESIAN_POINT('Ctrl Pts',(7.58606188694604,8.,-2.87863845879425));
#33184=CARTESIAN_POINT('Ctrl Pts',(8.01031931069726,8.,-0.146652009457745));
#33185=CARTESIAN_POINT('Ctrl Pts',(7.71659810676505,8.,2.4083107049283));
#33186=CARTESIAN_POINT('Ctrl Pts',(7.19805613432617,8.,4.27879853380268));
#33187=CARTESIAN_POINT('Ctrl Pts',(7.65938992538726,7.69401141008081,4.44213955875821));
#33188=CARTESIAN_POINT('Ctrl Pts',(7.58256899052929,7.74503701931255,4.41481449926364));
#33189=CARTESIAN_POINT('Ctrl Pts',(7.50571689117867,7.79604676496941,4.38754168444993));
#33190=CARTESIAN_POINT('Ctrl Pts',(7.35193866587471,7.89804240208479,4.33309620458235));
#33191=CARTESIAN_POINT('Ctrl Pts',(7.27500990494514,7.94903002495543,4.30592263479751));
#33192=CARTESIAN_POINT('Ctrl Pts',(7.1980528062913,8.,4.27880215351649));
#33193=CARTESIAN_POINT('Ctrl Pts',(7.65938992538726,7.69401141008081,4.44213955875821));
#33194=CARTESIAN_POINT('Ctrl Pts',(7.94257793183433,7.69786906181355,3.45561144714631));
#33195=CARTESIAN_POINT('Ctrl Pts',(8.129867747616,7.70112374147377,2.57269689084528));
#33196=CARTESIAN_POINT('Ctrl Pts',(8.23539599829409,7.70319454879578,1.73277853167637));
#33197=CARTESIAN_POINT('Origin',(7.68856688596016,0.,0.));
#33198=CARTESIAN_POINT('Origin',(7.68856688596016,0.,0.));
#33199=CARTESIAN_POINT('Ctrl Pts',(7.65938992538726,7.69401141008081,-4.44213955875821));
#33200=CARTESIAN_POINT('Ctrl Pts',(7.94257793183433,6.84158182974378,-4.93874443896366));
#33201=CARTESIAN_POINT('Ctrl Pts',(8.12551492847749,6.07927747400524,-5.38282408477123));
#33202=CARTESIAN_POINT('Ctrl Pts',(8.23006777285462,5.35342714305933,-5.80433017637318));
#33203=CARTESIAN_POINT('Origin',(7.68856688596016,0.,0.));
#33204=CARTESIAN_POINT('',(7.65938992538726,-5.37411354087801E-15,-8.88427911751642));
#33205=CARTESIAN_POINT('Ctrl Pts',(7.65938992538726,-6.93889390390723E-15,
-8.88427911751642));
#33206=CARTESIAN_POINT('Ctrl Pts',(7.94257793183433,-0.856287232069766,
-8.39435588610997));
#33207=CARTESIAN_POINT('Ctrl Pts',(8.12551492847749,-1.62202366451198,-7.95622077152864));
#33208=CARTESIAN_POINT('Ctrl Pts',(8.23006777285462,-2.34998381316212,-7.53836899138511));
#33209=CARTESIAN_POINT('Ctrl Pts',(8.2352995588869,2.35098758456643,-7.53754173724812));
#33210=CARTESIAN_POINT('Ctrl Pts',(8.12981699914252,1.62255181442061,-7.9557121398577));
#33211=CARTESIAN_POINT('Ctrl Pts',(7.94257793183433,0.85628723206971,-8.39435588610998));
#33212=CARTESIAN_POINT('Ctrl Pts',(7.65938992538726,-3.05311331771918E-15,
-8.88427911751642));
#33213=CARTESIAN_POINT('Origin',(7.68856688596016,0.,0.));
#33214=CARTESIAN_POINT('',(7.65938992538726,-7.69401141008081,-4.44213955875821));
#33215=CARTESIAN_POINT('Ctrl Pts',(7.65938992538726,-7.69401141008081,-4.44213955875821));
#33216=CARTESIAN_POINT('Ctrl Pts',(7.94257793183434,-7.69786906181355,-3.45561144714631));
#33217=CARTESIAN_POINT('Ctrl Pts',(8.12558259310879,-7.70129982645112,-2.57338080520902));
#33218=CARTESIAN_POINT('Ctrl Pts',(8.23018478415036,-7.70340868728785,-1.73401135132049));
#33219=CARTESIAN_POINT('Ctrl Pts',(8.2352995588869,-5.35220883425914,-5.8047858408404));
#33220=CARTESIAN_POINT('Ctrl Pts',(8.12981699914252,-6.07857291110272,-5.38302716017364));
#33221=CARTESIAN_POINT('Ctrl Pts',(7.94257793183433,-6.84158182974382,-4.93874443896362));
#33222=CARTESIAN_POINT('Ctrl Pts',(7.65938992538726,-7.69401141008081,-4.44213955875821));
#33223=CARTESIAN_POINT('Origin',(7.68856688596016,0.,0.));
#33224=CARTESIAN_POINT('',(7.65938992538726,-7.69401141008081,4.44213955875821));
#33225=CARTESIAN_POINT('Ctrl Pts',(7.65938992538726,-7.69401141008081,4.44213955875821));
#33226=CARTESIAN_POINT('Ctrl Pts',(7.94257793183433,-6.84158182974379,4.93874443896366));
#33227=CARTESIAN_POINT('Ctrl Pts',(8.12981699914252,-6.07857291110267,5.38302716017369));
#33228=CARTESIAN_POINT('Ctrl Pts',(8.2352995588869,-5.3522088342591,5.80478584084045));
#33229=CARTESIAN_POINT('Ctrl Pts',(8.23539599829409,-7.70319454879577,1.73277853167643));
#33230=CARTESIAN_POINT('Ctrl Pts',(8.12986774761599,-7.70112374147376,2.57269689084535));
#33231=CARTESIAN_POINT('Ctrl Pts',(7.94257793183433,-7.69786906181353,3.45561144714636));
#33232=CARTESIAN_POINT('Ctrl Pts',(7.65938992538726,-7.69401141008081,4.44213955875821));
#33233=CARTESIAN_POINT('Origin',(7.68856688596016,0.,0.));
#33234=CARTESIAN_POINT('Ctrl Pts',(8.23006777285462,-2.34998381316205,7.53836899138514));
#33235=CARTESIAN_POINT('Ctrl Pts',(8.12551492847749,-1.62202366451191,7.95622077152867));
#33236=CARTESIAN_POINT('Ctrl Pts',(7.94257793183433,-0.856287232069709,
8.39435588610998));
#33237=CARTESIAN_POINT('Ctrl Pts',(7.65938992538726,5.55111512312578E-15,
8.88427911751642));
#33238=CARTESIAN_POINT('Ctrl Pts',(7.18908433792779,7.73350218325398,-4.77266473975377));
#33239=CARTESIAN_POINT('Ctrl Pts',(7.58326629775444,6.50852271611219,-5.47990696485985));
#33240=CARTESIAN_POINT('Ctrl Pts',(8.01233031911798,4.12656046255355,-6.85513351315146));
#33241=CARTESIAN_POINT('Ctrl Pts',(7.71466028436332,1.89980377293487,-8.1407520873226));
#33242=CARTESIAN_POINT('Ctrl Pts',(7.1890843379278,0.266497816746022,-9.08374172079725));
#33243=CARTESIAN_POINT('Ctrl Pts',(7.34585286708095,7.72033859219626,-4.66248967942192));
#33244=CARTESIAN_POINT('Ctrl Pts',(7.74659985034045,6.48841258573789,-5.37591253016962));
#33245=CARTESIAN_POINT('Ctrl Pts',(8.18799973158063,4.08119252444856,-6.76996872254409));
#33246=CARTESIAN_POINT('Ctrl Pts',(7.88018217809361,1.82273896531981,-8.07036379730134));
#33247=CARTESIAN_POINT('Ctrl Pts',(7.34585286708095,0.177665211164014,-9.0172541863703));
#33248=CARTESIAN_POINT('Ctrl Pts',(7.5026213962341,7.70717500113853,-4.55231461909007));
#33249=CARTESIAN_POINT('Ctrl Pts',(7.90993340292647,6.4683024553636,-5.2719180954794));
#33250=CARTESIAN_POINT('Ctrl Pts',(8.36366914404328,4.03582458634359,-6.68480393193673));
#33251=CARTESIAN_POINT('Ctrl Pts',(8.0457040718239,1.74567415770476,-7.99997550728009));
#33252=CARTESIAN_POINT('Ctrl Pts',(7.50262139623411,0.0888326055820055,
-8.95076665194336));
#33253=CARTESIAN_POINT('Ctrl Pts',(7.65938992538726,7.69401141008081,-4.44213955875821));
#33254=CARTESIAN_POINT('Ctrl Pts',(8.07326695551249,6.4481923249893,-5.16792366078917));
#33255=CARTESIAN_POINT('Ctrl Pts',(8.53933855650593,3.9904566482386,-6.59963914132936));
#33256=CARTESIAN_POINT('Ctrl Pts',(8.21122596555418,1.66860935008971,-7.92958721725884));
#33257=CARTESIAN_POINT('Ctrl Pts',(7.65938992538726,-3.05311331771918E-15,
-8.88427911751642));
#33258=CARTESIAN_POINT('',(7.1980528062909,0.294448637285861,-9.0676043070345));
#33259=CARTESIAN_POINT('Ctrl Pts',(7.1980528062909,0.29444863728586,-9.0676043070345));
#33260=CARTESIAN_POINT('Ctrl Pts',(7.27501095230383,0.245475957519695,-9.03702283825866));
#33261=CARTESIAN_POINT('Ctrl Pts',(7.35194075984032,0.196448476343717,-9.00645263056793));
#33262=CARTESIAN_POINT('Ctrl Pts',(7.5057189835217,0.0982994861627256,-8.94534455832922));
#33263=CARTESIAN_POINT('Ctrl Pts',(7.58257003626746,0.0491763308674533,
-8.91480564605423));
#33264=CARTESIAN_POINT('Ctrl Pts',(7.65938992538726,-1.42870104749273E-15,
-8.88427911751642));
#33265=CARTESIAN_POINT('',(7.19805280629066,7.70555136271329,-4.78880215351701));
#33266=CARTESIAN_POINT('Ctrl Pts',(7.19805611451105,0.294451775473735,-9.06760249520089));
#33267=CARTESIAN_POINT('Ctrl Pts',(7.71659579227932,1.91434214917355,-8.13235835188762));
#33268=CARTESIAN_POINT('Ctrl Pts',(8.009965927807,4.12706541575281,-6.85484197828594));
#33269=CARTESIAN_POINT('Ctrl Pts',(7.58605957246042,6.49297443347419,-5.48888377002634));
#33270=CARTESIAN_POINT('Ctrl Pts',(7.19805432694391,7.70554842326237,-4.78880385060979));
#33271=CARTESIAN_POINT('Ctrl Pts',(7.65938992538726,7.69401141008081,-4.44213955875821));
#33272=CARTESIAN_POINT('Ctrl Pts',(7.58256899052918,7.69586001901446,-4.49999156234384));
#33273=CARTESIAN_POINT('Ctrl Pts',(7.50571689117887,7.6977459413815,-4.55780370532989));
#33274=CARTESIAN_POINT('Ctrl Pts',(7.35193866587394,7.70159259125265,-4.6733572580815));
#33275=CARTESIAN_POINT('Ctrl Pts',(7.27500990494294,7.70355340094283,-4.73110061965955));
#33276=CARTESIAN_POINT('Ctrl Pts',(7.1980528062913,7.70555136271284,-4.78880215351727));
#33277=CARTESIAN_POINT('Origin',(8.4,0.,0.));
#33278=CARTESIAN_POINT('',(8.4,-5.37,6.57635331142129E-16));
#33279=CARTESIAN_POINT('Origin',(8.4,0.,0.));
#33280=CARTESIAN_POINT('Origin',(7.1980528062909,8.,-4.27880215351799));
#33281=CARTESIAN_POINT('',(7.19805280629066,8.,-4.27880215351701));
#33282=CARTESIAN_POINT('Origin',(7.65938992538726,-5.37411354087801E-15,
-8.88427911751642));
#33283=CARTESIAN_POINT('',(7.19805280629066,-0.294448637286711,-9.06760430703401));
#33284=CARTESIAN_POINT('Ctrl Pts',(7.65938992538726,-7.34681978757065E-15,
-8.88427911751642));
#33285=CARTESIAN_POINT('Ctrl Pts',(7.58256899052983,-0.0491770002977431,
-8.91480606160718));
#33286=CARTESIAN_POINT('Ctrl Pts',(7.50571689118011,-0.0983008235869914,
-8.94534538977939));
#33287=CARTESIAN_POINT('Ctrl Pts',(7.35193866587446,-0.196449810832315,
-9.00645346266337));
#33288=CARTESIAN_POINT('Ctrl Pts',(7.27500990494381,-0.245476624013499,
-9.03702325445593));
#33289=CARTESIAN_POINT('Ctrl Pts',(7.1980528062913,-0.294448637287159,-9.06760430703376));
#33290=CARTESIAN_POINT('',(7.19805280629066,0.294448637286708,-9.06760430703401));
#33291=CARTESIAN_POINT('Origin',(7.1980528062909,7.70555136271414,4.78880215351652));
#33292=CARTESIAN_POINT('',(7.19805280629066,7.70555136271329,4.78880215351701));
#33293=CARTESIAN_POINT('Origin',(7.65938992538726,-7.69401141008081,-4.44213955875821));
#33294=CARTESIAN_POINT('',(7.1980528062909,-7.70555136271414,-4.78880215351652));
#33295=CARTESIAN_POINT('Ctrl Pts',(7.1980528062909,-7.70555136271414,-4.78880215351652));
#33296=CARTESIAN_POINT('Ctrl Pts',(7.27501095229772,-7.70355337375246,-4.73109983436428));
#33297=CARTESIAN_POINT('Ctrl Pts',(7.35194075983702,-7.70159253788124,-4.67335568633486));
#33298=CARTESIAN_POINT('Ctrl Pts',(7.50571898352358,-7.69774589003658,-4.55780213135908));
#33299=CARTESIAN_POINT('Ctrl Pts',(7.58257003626834,-7.69585999385016,-4.49999077482257));
#33300=CARTESIAN_POINT('Ctrl Pts',(7.65938992538726,-7.69401141008081,-4.44213955875821));
#33301=CARTESIAN_POINT('',(7.19805280629065,-8.,-4.27880215351701));
#33302=CARTESIAN_POINT('Ctrl Pts',(7.65938992538726,-7.69401141008081,-4.44213955875821));
#33303=CARTESIAN_POINT('Ctrl Pts',(7.58256899053098,-7.74503701931143,-4.41481449926424));
#33304=CARTESIAN_POINT('Ctrl Pts',(7.50571689118228,-7.79604676496702,-4.3875416844512));
#33305=CARTESIAN_POINT('Ctrl Pts',(7.35193866587007,-7.89804240208786,-4.3330962045807));
#33306=CARTESIAN_POINT('Ctrl Pts',(7.27500990493544,-7.94903002496185,-4.30592263479409));
#33307=CARTESIAN_POINT('Ctrl Pts',(7.1980528062913,-8.,-4.27880215351649));
#33308=CARTESIAN_POINT('',(7.19805280629066,-7.70555136271329,-4.78880215351701));
#33309=CARTESIAN_POINT('Origin',(7.1980528062909,-0.294448637285862,9.0676043070345));
#33310=CARTESIAN_POINT('',(7.1980528062909,-0.294448637285862,9.0676043070345));
#33311=CARTESIAN_POINT('',(7.19805280629066,-0.294448637286709,9.06760430703401));
#33312=CARTESIAN_POINT('Ctrl Pts',(7.1980528062909,-0.294448637285858,9.0676043070345));
#33313=CARTESIAN_POINT('Ctrl Pts',(7.27501095230018,-0.245475957522012,
9.03702283826011));
#33314=CARTESIAN_POINT('Ctrl Pts',(7.35194075983832,-0.196448476344994,
9.00645263056873));
#33315=CARTESIAN_POINT('Ctrl Pts',(7.50571898351829,-0.0982994861648936,
8.94534455833057));
#33316=CARTESIAN_POINT('Ctrl Pts',(7.58257003626595,-0.0491763308684156,
8.91480564605483));
#33317=CARTESIAN_POINT('Ctrl Pts',(7.65938992538726,6.46212393927782E-15,
8.88427911751642));
#33318=CARTESIAN_POINT('Origin',(7.65938992538726,-7.69401141008081,4.44213955875821));
#33319=CARTESIAN_POINT('',(7.19805280629089,-8.,4.27880215351799));
#33320=CARTESIAN_POINT('Ctrl Pts',(7.1980528062909,-8.,4.27880215351798));
#33321=CARTESIAN_POINT('Ctrl Pts',(7.27501095230383,-7.949029331272,4.30592300389896));
#33322=CARTESIAN_POINT('Ctrl Pts',(7.35194075984076,-7.89804101422459,4.33309694423571));
#33323=CARTESIAN_POINT('Ctrl Pts',(7.50571898352634,-7.79604537619627,4.38754242697037));
#33324=CARTESIAN_POINT('Ctrl Pts',(7.58257003626946,-7.7450363247163,4.4148148712317));
#33325=CARTESIAN_POINT('Ctrl Pts',(7.65938992538726,-7.69401141008081,4.44213955875821));
#33326=CARTESIAN_POINT('',(7.19805280629065,-7.70555136271329,4.78880215351701));
#33327=CARTESIAN_POINT('Ctrl Pts',(7.65938992538726,-7.69401141008081,4.44213955875821));
#33328=CARTESIAN_POINT('Ctrl Pts',(7.58256899052981,-7.69586001901445,4.49999156234336));
#33329=CARTESIAN_POINT('Ctrl Pts',(7.50571689117983,-7.69774594138148,4.55780370532917));
#33330=CARTESIAN_POINT('Ctrl Pts',(7.35193866587556,-7.70159259125261,4.67335725808028));
#33331=CARTESIAN_POINT('Ctrl Pts',(7.2750099049467,-7.70355340094273,4.73110061965673));
#33332=CARTESIAN_POINT('Ctrl Pts',(7.1980528062913,-7.70555136271284,4.78880215351727));
#33333=CARTESIAN_POINT('',(7.19805280629067,-8.,4.27880215351701));
#33334=CARTESIAN_POINT('Ctrl Pts',(7.18908433792779,-7.73350218325399,4.77266473975376));
#33335=CARTESIAN_POINT('Ctrl Pts',(7.71466028436332,-6.10019622706492,5.71565437322854));
#33336=CARTESIAN_POINT('Ctrl Pts',(8.01233031911798,-3.87343953744612,7.00127294739976));
#33337=CARTESIAN_POINT('Ctrl Pts',(7.58326629775444,-1.49147728388766,8.37649949569126));
#33338=CARTESIAN_POINT('Ctrl Pts',(7.1890843379278,-0.266497816746021,9.08374172079725));
#33339=CARTESIAN_POINT('Ctrl Pts',(7.34585286708095,-7.72033859219626,4.66248967942191));
#33340=CARTESIAN_POINT('Ctrl Pts',(7.88018217809362,-6.0777705835851,5.61372014708552));
#33341=CARTESIAN_POINT('Ctrl Pts',(8.18799973158063,-3.82236863432465,6.91940076517984));
#33342=CARTESIAN_POINT('Ctrl Pts',(7.74659985034044,-1.41147052678086,8.30708639456859));
#33343=CARTESIAN_POINT('Ctrl Pts',(7.34585286708095,-0.177665211164012,
9.01725418637031));
#33344=CARTESIAN_POINT('Ctrl Pts',(7.5026213962341,-7.70717500113854,4.55231461909006));
#33345=CARTESIAN_POINT('Ctrl Pts',(8.04570407182393,-6.05534494010528,5.5117859209425));
#33346=CARTESIAN_POINT('Ctrl Pts',(8.36366914404327,-3.77129773120317,6.83752858295992));
#33347=CARTESIAN_POINT('Ctrl Pts',(7.90993340292645,-1.33146376967407,8.23767329344591));
#33348=CARTESIAN_POINT('Ctrl Pts',(7.5026213962341,-0.0888326055820031,
8.95076665194336));
#33349=CARTESIAN_POINT('Ctrl Pts',(7.65938992538726,-7.69401141008081,4.44213955875821));
#33350=CARTESIAN_POINT('Ctrl Pts',(8.21122596555423,-6.03291929662547,5.40985169479948));
#33351=CARTESIAN_POINT('Ctrl Pts',(8.53933855650592,-3.7202268280817,6.75565640074));
#33352=CARTESIAN_POINT('Ctrl Pts',(8.07326695551245,-1.25145701256728,8.16826019232323));
#33353=CARTESIAN_POINT('Ctrl Pts',(7.65938992538726,5.55111512312578E-15,
8.88427911751642));
#33354=CARTESIAN_POINT('Ctrl Pts',(7.19805432694369,-0.294451576736895,
9.06760260994166));
#33355=CARTESIAN_POINT('Ctrl Pts',(7.58605957246035,-1.50702556652525,8.36752269052502));
#33356=CARTESIAN_POINT('Ctrl Pts',(8.00996592780699,-3.87293458424645,7.00156448226551));
#33357=CARTESIAN_POINT('Ctrl Pts',(7.71659579227937,-6.08565785082586,5.72404810866374));
#33358=CARTESIAN_POINT('Ctrl Pts',(7.19805611451127,-7.70554822452553,4.78880396535056));
#33359=CARTESIAN_POINT('Origin',(0.,-7.85277568135665,4.53380215351701));
#33360=CARTESIAN_POINT('',(0.849339335588243,-7.70555136271329,4.78880215351701));
#33361=CARTESIAN_POINT('',(0.849339335588256,-8.,4.27880215351701));
#33362=CARTESIAN_POINT('Ctrl Pts',(0.849339335588243,-7.70555136271329,
4.78880215351701));
#33363=CARTESIAN_POINT('Ctrl Pts',(0.843815452152285,-7.85277568135665,
4.53380215351701));
#33364=CARTESIAN_POINT('Ctrl Pts',(0.849339335588256,-8.,4.27880215351701));
#33365=CARTESIAN_POINT('',(0.,-8.,4.27880215351701));
#33366=CARTESIAN_POINT('',(0.,-7.70555136271329,4.78880215351701));
#33367=CARTESIAN_POINT('Ctrl Pts',(7.18908433792779,-8.,-4.31107698104349));
#33368=CARTESIAN_POINT('Ctrl Pts',(7.58326629775444,-8.,-2.89659253083133));
#33369=CARTESIAN_POINT('Ctrl Pts',(8.01268601649393,-8.,-0.14606847802109));
#33370=CARTESIAN_POINT('Ctrl Pts',(7.71466028436332,-8.,2.42509771409418));
#33371=CARTESIAN_POINT('Ctrl Pts',(7.1890843379278,-8.,4.31107698104348));
#33372=CARTESIAN_POINT('Ctrl Pts',(7.34585286708095,-7.89800380336027,-4.3547645069484));
#33373=CARTESIAN_POINT('Ctrl Pts',(7.74659985034045,-7.89988311251892,-2.93117386439888));
#33374=CARTESIAN_POINT('Ctrl Pts',(8.18834927452041,-7.90355897903611,-0.149358354443497));
#33375=CARTESIAN_POINT('Ctrl Pts',(7.88018217809361,-7.90050954890512,2.45664365021595));
#33376=CARTESIAN_POINT('Ctrl Pts',(7.34585286708096,-7.89800380336027,4.35476450694839));
#33377=CARTESIAN_POINT('Ctrl Pts',(7.5026213962341,-7.79600760672054,-4.3984520328533));
#33378=CARTESIAN_POINT('Ctrl Pts',(7.90993340292647,-7.79976622503783,-2.96575519796644));
#33379=CARTESIAN_POINT('Ctrl Pts',(8.36401253254689,-7.80711795807223,-0.152648230865896));
#33380=CARTESIAN_POINT('Ctrl Pts',(8.04570407182389,-7.80101909781024,2.48818958633772));
#33381=CARTESIAN_POINT('Ctrl Pts',(7.50262139623411,-7.79600760672054,4.3984520328533));
#33382=CARTESIAN_POINT('Ctrl Pts',(7.65938992538726,-7.69401141008081,-4.44213955875821));
#33383=CARTESIAN_POINT('Ctrl Pts',(8.07326695551249,-7.69964933755674,-3.000336531534));
#33384=CARTESIAN_POINT('Ctrl Pts',(8.53967579057338,-7.71067693710834,-0.155938107288303));
#33385=CARTESIAN_POINT('Ctrl Pts',(8.21122596555418,-7.70152864671536,2.51973552245949));
#33386=CARTESIAN_POINT('Ctrl Pts',(7.65938992538726,-7.69401141008081,4.44213955875821));
#33387=CARTESIAN_POINT('Ctrl Pts',(7.19805613432595,-8.,4.27879853380353));
#33388=CARTESIAN_POINT('Ctrl Pts',(7.716598106765,-8.,2.40831070492898));
#33389=CARTESIAN_POINT('Ctrl Pts',(8.01031931069726,-8.,-0.146652009456896));
#33390=CARTESIAN_POINT('Ctrl Pts',(7.5860618869461,-8.,-2.87863845879359));
#33391=CARTESIAN_POINT('Ctrl Pts',(7.19805435334694,-8.,-4.27879875406444));
#33392=CARTESIAN_POINT('Origin',(0.,7.63278329429795E-16,9.06760430703401));
#33393=CARTESIAN_POINT('',(0.849339335588243,0.294448637286709,9.06760430703401));
#33394=CARTESIAN_POINT('',(0.849339335588255,-0.294448637286709,9.06760430703401));
#33395=CARTESIAN_POINT('Ctrl Pts',(0.849339335588243,0.294448637286709,
9.06760430703401));
#33396=CARTESIAN_POINT('Ctrl Pts',(0.843815452152285,-2.77555756156289E-16,
9.06760430703401));
#33397=CARTESIAN_POINT('Ctrl Pts',(0.849339335588255,-0.294448637286709,
9.06760430703402));
#33398=CARTESIAN_POINT('',(0.,-0.294448637286709,9.06760430703401));
#33399=CARTESIAN_POINT('',(0.,0.29444863728671,9.06760430703401));
#33400=CARTESIAN_POINT('Origin',(0.,-7.85277568135665,-4.53380215351701));
#33401=CARTESIAN_POINT('',(0.849339335588243,-8.,-4.27880215351701));
#33402=CARTESIAN_POINT('',(0.849339335588255,-7.70555136271329,-4.78880215351701));
#33403=CARTESIAN_POINT('Ctrl Pts',(0.849339335588243,-8.,-4.27880215351701));
#33404=CARTESIAN_POINT('Ctrl Pts',(0.843815452152285,-7.85277568135665,
-4.53380215351701));
#33405=CARTESIAN_POINT('Ctrl Pts',(0.849339335588255,-7.70555136271329,
-4.78880215351701));
#33406=CARTESIAN_POINT('',(0.,-7.70555136271329,-4.78880215351701));
#33407=CARTESIAN_POINT('',(0.,-8.,-4.27880215351701));
#33408=CARTESIAN_POINT('Ctrl Pts',(7.18908433792779,-0.266497816746021,
-9.08374172079725));
#33409=CARTESIAN_POINT('Ctrl Pts',(7.58326629775444,-1.49147728388782,-8.37649949569117));
#33410=CARTESIAN_POINT('Ctrl Pts',(8.01233031911798,-3.87343953744646,-7.00127294739956));
#33411=CARTESIAN_POINT('Ctrl Pts',(7.71466028436332,-6.10019622706513,-5.71565437322842));
#33412=CARTESIAN_POINT('Ctrl Pts',(7.1890843379278,-7.73350218325398,-4.77266473975377));
#33413=CARTESIAN_POINT('Ctrl Pts',(7.34585286708095,-0.177665211164016,
-9.01725418637031));
#33414=CARTESIAN_POINT('Ctrl Pts',(7.74659985034045,-1.41147052678103,-8.3070863945685));
#33415=CARTESIAN_POINT('Ctrl Pts',(8.18799973158063,-3.82236863432499,-6.91940076517965));
#33416=CARTESIAN_POINT('Ctrl Pts',(7.88018217809361,-6.0777705835853,-5.6137201470854));
#33417=CARTESIAN_POINT('Ctrl Pts',(7.34585286708095,-7.72033859219626,-4.66248967942192));
#33418=CARTESIAN_POINT('Ctrl Pts',(7.5026213962341,-0.0888326055820114,
-8.95076665194336));
#33419=CARTESIAN_POINT('Ctrl Pts',(7.90993340292647,-1.33146376967424,-8.23767329344583));
#33420=CARTESIAN_POINT('Ctrl Pts',(8.36366914404328,-3.77129773120352,-6.83752858295973));
#33421=CARTESIAN_POINT('Ctrl Pts',(8.0457040718239,-6.05534494010547,-5.51178592094237));
#33422=CARTESIAN_POINT('Ctrl Pts',(7.50262139623411,-7.70717500113853,-4.55231461909006));
#33423=CARTESIAN_POINT('Ctrl Pts',(7.65938992538726,-6.93889390390723E-15,
-8.88427911751642));
#33424=CARTESIAN_POINT('Ctrl Pts',(8.07326695551249,-1.25145701256745,-8.16826019232316));
#33425=CARTESIAN_POINT('Ctrl Pts',(8.53933855650593,-3.72022682808205,-6.75565640073981));
#33426=CARTESIAN_POINT('Ctrl Pts',(8.21122596555418,-6.03291929662565,-5.40985169479935));
#33427=CARTESIAN_POINT('Ctrl Pts',(7.65938992538726,-7.69401141008081,-4.44213955875821));
#33428=CARTESIAN_POINT('Ctrl Pts',(7.19805611451105,-7.70554822452627,-4.78880396535013));
#33429=CARTESIAN_POINT('Ctrl Pts',(7.71659579227932,-6.08565785082645,-5.7240481086634));
#33430=CARTESIAN_POINT('Ctrl Pts',(8.00996592780701,-3.87293458424719,-7.00156448226509));
#33431=CARTESIAN_POINT('Ctrl Pts',(7.58605957246042,-1.50702556652582,-8.36752269052469));
#33432=CARTESIAN_POINT('Ctrl Pts',(7.19805432694391,-0.294451576737634,
-9.06760260994123));
#33433=CARTESIAN_POINT('Origin',(0.,7.85277568135665,4.53380215351701));
#33434=CARTESIAN_POINT('',(0.849339335588243,8.,4.27880215351701));
#33435=CARTESIAN_POINT('',(0.849339335588254,7.70555136271329,4.78880215351701));
#33436=CARTESIAN_POINT('Ctrl Pts',(0.849339335588243,8.,4.27880215351701));
#33437=CARTESIAN_POINT('Ctrl Pts',(0.843815452152285,7.85277568135665,4.53380215351701));
#33438=CARTESIAN_POINT('Ctrl Pts',(0.849339335588254,7.70555136271329,4.78880215351701));
#33439=CARTESIAN_POINT('',(0.,7.70555136271329,4.78880215351701));
#33440=CARTESIAN_POINT('',(0.,8.,4.27880215351701));
#33441=CARTESIAN_POINT('Origin',(0.,-1.2490009027033E-15,-9.06760430703401));
#33442=CARTESIAN_POINT('',(0.849339335588244,-0.294448637286709,-9.06760430703401));
#33443=CARTESIAN_POINT('',(0.849339335588254,0.294448637286709,-9.06760430703401));
#33444=CARTESIAN_POINT('Ctrl Pts',(0.849339335588244,-0.294448637286709,
-9.06760430703401));
#33445=CARTESIAN_POINT('Ctrl Pts',(0.843815452152285,1.73472347597681E-16,
-9.06760430703401));
#33446=CARTESIAN_POINT('Ctrl Pts',(0.849339335588254,0.294448637286709,
-9.06760430703402));
#33447=CARTESIAN_POINT('',(0.,0.294448637286708,-9.06760430703401));
#33448=CARTESIAN_POINT('',(0.,-0.294448637286711,-9.06760430703401));
#33449=CARTESIAN_POINT('Origin',(0.,7.85277568135664,-4.53380215351701));
#33450=CARTESIAN_POINT('',(0.849339335588243,7.70555136271329,-4.78880215351701));
#33451=CARTESIAN_POINT('',(0.849339335588255,8.,-4.27880215351701));
#33452=CARTESIAN_POINT('Ctrl Pts',(0.849339335588243,7.70555136271329,-4.78880215351701));
#33453=CARTESIAN_POINT('Ctrl Pts',(0.843815452152285,7.85277568135665,-4.53380215351701));
#33454=CARTESIAN_POINT('Ctrl Pts',(0.849339335588255,8.,-4.27880215351701));
#33455=CARTESIAN_POINT('',(0.,8.,-4.27880215351701));
#33456=CARTESIAN_POINT('',(0.,7.70555136271329,-4.78880215351701));
#33457=CARTESIAN_POINT('Origin',(0.,8.,4.61880215351701));
#33458=CARTESIAN_POINT('Ctrl Pts',(0.849339335588254,7.70555136271329,4.78880215351701));
#33459=CARTESIAN_POINT('Ctrl Pts',(-0.317120580865619,3.99999999999977,
6.92820323027565));
#33460=CARTESIAN_POINT('Ctrl Pts',(0.849339335588243,0.294448637286709,
9.06760430703402));
#33461=CARTESIAN_POINT('Origin',(0.,8.,-4.61880215351701));
#33462=CARTESIAN_POINT('Ctrl Pts',(0.849339335588255,8.,-4.27880215351701));
#33463=CARTESIAN_POINT('Ctrl Pts',(-0.317120580865621,8.,2.63122856836162E-13));
#33464=CARTESIAN_POINT('Ctrl Pts',(0.849339335588243,8.,4.27880215351701));
#33465=CARTESIAN_POINT('Origin',(0.,-1.69692038195985E-15,-9.23760430703401));
#33466=CARTESIAN_POINT('Ctrl Pts',(0.849339335588254,0.294448637286709,
-9.06760430703402));
#33467=CARTESIAN_POINT('Ctrl Pts',(-0.317120580865621,4.00000000000023,
-6.92820323027538));
#33468=CARTESIAN_POINT('Ctrl Pts',(0.849339335588243,7.70555136271329,-4.78880215351701));
#33469=CARTESIAN_POINT('Origin',(0.711433114039842,0.,0.));
#33470=CARTESIAN_POINT('',(0.,-7.60300281800529,9.31099306497849E-16));
#33471=CARTESIAN_POINT('Origin',(0.,0.,0.));
#33472=CARTESIAN_POINT('',(0.229474401962219,-8.,-9.15987121259293E-16));
#33473=CARTESIAN_POINT('',(0.711433114039842,-8.83380215351701,-1.08182875316056E-15));
#33474=CARTESIAN_POINT('Ctrl Pts',(0.849339335588256,-8.,4.27880215351701));
#33475=CARTESIAN_POINT('Ctrl Pts',(0.229474401962242,-8.,2.00501685195949));
#33476=CARTESIAN_POINT('Ctrl Pts',(0.229474401962219,-8.,-8.52256803200703E-16));
#33477=CARTESIAN_POINT('Ctrl Pts',(0.849339335588255,-0.294448637286709,
9.06760430703402));
#33478=CARTESIAN_POINT('Ctrl Pts',(-0.31712058086562,-4.00000000000023,
6.92820323027538));
#33479=CARTESIAN_POINT('Ctrl Pts',(0.849339335588243,-7.70555136271329,
4.78880215351701));
#33480=CARTESIAN_POINT('Ctrl Pts',(0.849339335588255,-7.70555136271329,
-4.78880215351701));
#33481=CARTESIAN_POINT('Ctrl Pts',(-0.317120580865619,-3.99999999999977,
-6.92820323027564));
#33482=CARTESIAN_POINT('Ctrl Pts',(0.849339335588244,-0.294448637286708,
-9.06760430703401));
#33483=CARTESIAN_POINT('Ctrl Pts',(0.229474401962219,-8.,-8.52256803200703E-16));
#33484=CARTESIAN_POINT('Ctrl Pts',(0.229474401962195,-8.,-2.00501685195963));
#33485=CARTESIAN_POINT('Ctrl Pts',(0.849339335588243,-8.,-4.27880215351701));
#33486=CARTESIAN_POINT('Origin',(0.15,0.,0.));
#33487=CARTESIAN_POINT('',(0.,-5.37,-6.57635331142129E-16));
#33488=CARTESIAN_POINT('Origin',(0.,0.,0.));
#33489=CARTESIAN_POINT('',(0.4,-5.05,-6.18446633569413E-16));
#33490=CARTESIAN_POINT('',(0.15,-5.25,-6.42939569552361E-16));
#33491=CARTESIAN_POINT('Origin',(0.4,0.,0.));
#33492=CARTESIAN_POINT('Origin',(4.2,0.,0.));
#33493=CARTESIAN_POINT('',(8.,-5.05,-6.18446633569413E-16));
#33494=CARTESIAN_POINT('',(4.2,-5.05,-6.18446633569413E-16));
#33495=CARTESIAN_POINT('Origin',(8.,0.,0.));
#33496=CARTESIAN_POINT('Origin',(8.25,0.,0.));
#33497=CARTESIAN_POINT('',(8.25,-5.25,-6.42939569552361E-16));
#33498=CARTESIAN_POINT('Origin',(0.,-8.,-4.61880215351701));
#33499=CARTESIAN_POINT('Origin',(0.,-8.,4.61880215351701));
#33500=CARTESIAN_POINT('Origin',(0.,5.6564012731995E-16,9.23760430703401));
#33501=CARTESIAN_POINT('Origin',(0.,0.,0.));
#56605=UNCERTAINTY_MEASURE_WITH_UNIT(LENGTH_MEASURE(0.01),#56640,
'DISTANCE_ACCURACY_VALUE',
'Maximum model space distance between geometric entities at asserted c
onnectivities');
#56617=UNCERTAINTY_MEASURE_WITH_UNIT(LENGTH_MEASURE(0.01),#56640,
'DISTANCE_ACCURACY_VALUE',
'Maximum model space distance between geometric entities at asserted c
onnectivities');
#56627=(
GEOMETRIC_REPRESENTATION_CONTEXT(3)
GLOBAL_UNCERTAINTY_ASSIGNED_CONTEXT((#56605))
GLOBAL_UNIT_ASSIGNED_CONTEXT((#56640,#56642,#56643))
REPRESENTATION_CONTEXT('','3D')
);
#56639=(
GEOMETRIC_REPRESENTATION_CONTEXT(3)
GLOBAL_UNCERTAINTY_ASSIGNED_CONTEXT((#56617))
GLOBAL_UNIT_ASSIGNED_CONTEXT((#56640,#56642,#56643))
REPRESENTATION_CONTEXT('','3D')
);
#56640=(
LENGTH_UNIT()
NAMED_UNIT(*)
SI_UNIT(.MILLI.,.METRE.)
);
#56642=(
NAMED_UNIT(*)
PLANE_ANGLE_UNIT()
SI_UNIT($,.RADIAN.)
);
#56643=(
NAMED_UNIT(*)
SI_UNIT($,.STERADIAN.)
SOLID_ANGLE_UNIT()
);
#56653=SHAPE_DEFINITION_REPRESENTATION(#56674,#56753);
#56674=PRODUCT_DEFINITION_SHAPE('',$,#56775);
#56753=SHAPE_REPRESENTATION('',(#17774),#56627);
#56765=PRODUCT_DEFINITION_CONTEXT('part definition',#56830,'design');
#56775=PRODUCT_DEFINITION('2026-10-26-00-02-43-431',
'09_Hex_Nut_ISO_4032_M10',#56796,#56765);
#56796=PRODUCT_DEFINITION_FORMATION('',$,#56841);
#56830=APPLICATION_CONTEXT(
'Core Data for Automotive Mechanical Design Process');
#56831=PRODUCT_CONTEXT('part definition',#56830,'mechanical');
#56841=PRODUCT('2026-10-26-00-02-43-431','09_Hex_Nut_ISO_4032_M10',$,(#56831));
#56916=COLOUR_RGB('Black',0.12,0.14,0.17);
#56917=FILL_AREA_STYLE_COLOUR('',#56916);
#56918=FILL_AREA_STYLE('',(#56917));
#56919=SURFACE_STYLE_FILL_AREA(#56918);
#56920=SURFACE_SIDE_STYLE('',(#56919));
#56921=SURFACE_STYLE_USAGE(.BOTH.,#56920);
#56922=PRESENTATION_STYLE_ASSIGNMENT((#56921));
ENDSEC;
END-ISO-10303-21;
